ISO-10303-21;
HEADER;
FILE_DESCRIPTION (('STEP AP214'),
    '1' );
FILE_NAME ('Cross Recess Screw.step',
    '2026-10-07T18:46:32',
    ( '' ),
    ( '' ),
    'SwSTEP 2.0',
    'SolidWorks 2020',
    '' );
FILE_SCHEMA (( 'AUTOMOTIVE_DESIGN' ));
ENDSEC;

DATA;
#3=CARTESIAN_POINT ( 'NONE',  ( -8.638906393579159015, 44.91645089659918710, 70.88527860057354246 ) ) ;
#37=ORIENTED_EDGE ( 'NONE', *, *, #3463, .T. ) ;
#52=CIRCLE ( 'NONE', #8647, 0.9652499999999990532 ) ;
#65=CARTESIAN_POINT ( 'NONE',  ( -8.638906393579159015, 41.66638367286108746, 68.06527860057354928 ) ) ;
#84=DIRECTION ( 'NONE',  ( -1.224646799147353207E-16, -0.000000000000000000, -1.000000000000000000 ) ) ;
#105=DIRECTION ( 'NONE',  ( -1.000000000000000000, 0.000000000000000000, 0.000000000000000000 ) ) ;
#137=ORIENTED_EDGE ( 'NONE', *, *, #1060, .T. ) ;
#172=EDGE_CURVE ( 'NONE', #17257, #3651, #10302, .T. ) ;
#183=VERTEX_POINT ( 'NONE', #20371 ) ;
#190=CIRCLE ( 'NONE', #5215, 2.881677036926254765 ) ;
#201=DIRECTION ( 'NONE',  ( 1.000000000000000000, 0.000000000000000000, -1.224646799147353207E-16 ) ) ;
#208=CARTESIAN_POINT ( 'NONE',  ( -4.603906393579157097, 42.46645089659918426, 70.38908280829822672 ) ) ;
#243=ORIENTED_EDGE ( 'NONE', *, *, #4452, .F. ) ;
#244=DIRECTION ( 'NONE',  ( 1.000000000000000000, 0.000000000000000000, 0.000000000000000000 ) ) ;
#274=AXIS2_PLACEMENT_3D ( 'NONE', #12872, #19723, #18021 ) ;
#286=EDGE_LOOP ( 'NONE', ( #6678, #18938, #13760, #4067 ) ) ;
#299=VERTEX_POINT ( 'NONE', #20250 ) ;
#355=LINE ( 'NONE', #19056, #20802 ) ;
#377=CARTESIAN_POINT ( 'NONE',  ( -6.297229356652903398, 42.46645089659918426, 68.75385983073485363 ) ) ;
#412=VERTEX_POINT ( 'NONE', #4202 ) ;
#448=ADVANCED_FACE ( 'NONE', ( #17522 ), #612, .T. ) ;
#494=ORIENTED_EDGE ( 'NONE', *, *, #16304, .F. ) ;
#496=CARTESIAN_POINT ( 'NONE',  ( -9.178906393579158163, 42.46645089659918426, 74.06027860057353962 ) ) ;
#531=LINE ( 'NONE', #10629, #18304 ) ;
#538=VERTEX_POINT ( 'NONE', #2738 ) ;
#571=( LENGTH_UNIT ( ) NAMED_UNIT ( * ) SI_UNIT ( .MILLI., .METRE. ) );
#612=CYLINDRICAL_SURFACE ( 'NONE', #7393, 2.500000000000000444 ) ;
#616=TOROIDAL_SURFACE ( 'NONE', #20655, 3.750000000000000000, 1.250000000000000000 ) ;
#686=CARTESIAN_POINT ( 'NONE',  ( -8.134906293162368129, 43.00645089659919051, 68.06527860057354928 ) ) ;
#709=CARTESIAN_POINT ( 'NONE',  ( -8.638906393579159015, 43.26651812033729527, 68.06527860057354928 ) ) ;
#718=CARTESIAN_POINT ( 'NONE',  ( -9.178906393579158163, 42.46645089659918426, 68.06527860057354928 ) ) ;
#742=EDGE_LOOP ( 'NONE', ( #18223, #13014, #9930, #12285, #20664, #4144, #15061 ) ) ;
#807=FACE_OUTER_BOUND ( 'NONE', #742, .T. ) ;
#826=ORIENTED_EDGE ( 'NONE', *, *, #19386, .T. ) ;
#952=CONICAL_SURFACE ( 'NONE', #6348, 4.575000000000001066, 0.8028514559173934861 ) ;
#983=EDGE_CURVE ( 'NONE', #1254, #16141, #10054, .T. ) ;
#1024=ORIENTED_EDGE ( 'NONE', *, *, #14927, .T. ) ;
#1031=DIRECTION ( 'NONE',  ( -1.224646799147353207E-16, -0.000000000000000000, -1.000000000000000000 ) ) ;
#1036=B_SPLINE_CURVE_WITH_KNOTS ( 'NONE', 3,
 ( #16940, #11680, #11466, #18737 ),
 .UNSPECIFIED., .F., .F.,
 ( 4, 4 ),
 ( 0.001759598105097497350, 0.004588913567995311395 ),
 .UNSPECIFIED. ) ;
#1043=EDGE_CURVE ( 'NONE', #14452, #17182, #21467, .T. ) ;
#1058=ORIENTED_EDGE ( 'NONE', *, *, #9168, .F. ) ;
#1060=EDGE_CURVE ( 'NONE', #18170, #3171, #20681, .T. ) ;
#1086=CARTESIAN_POINT ( 'NONE',  ( -8.638906393579159015, 41.42245079618239600, 68.06527860057354928 ) ) ;
#1096=CARTESIAN_POINT ( 'NONE',  ( -10.20831163238817219, 41.92645089659918511, 70.88527860057354246 ) ) ;
#1113=DIRECTION ( 'NONE',  ( 2.343267634472166901E-16, 0.8949343913984426635, 0.4461977533474357771 ) ) ;
#1118=CARTESIAN_POINT ( 'NONE',  ( -9.718906393579157310, 41.58710221366784054, 69.00503344894293889 ) ) ;
#1127=DIRECTION ( 'NONE',  ( 1.000000000000000000, 0.000000000000000000, -1.224646799147353207E-16 ) ) ;
#1184=ORIENTED_EDGE ( 'NONE', *, *, #9168, .T. ) ;
#1195=VERTEX_POINT ( 'NONE', #17846 ) ;
#1203=ORIENTED_EDGE ( 'NONE', *, *, #17279, .F. ) ;
#1213=CARTESIAN_POINT ( 'NONE',  ( -9.178906393579158163, 42.46645089659918426, 68.06527860057354928 ) ) ;
#1237=DIRECTION ( 'NONE',  ( 0.000000000000000000, 0.000000000000000000, 1.000000000000000000 ) ) ;
#1254=VERTEX_POINT ( 'NONE', #16258 ) ;
#1255=CIRCLE ( 'NONE', #15897, 4.575000000000001066 ) ;
#1260=EDGE_LOOP ( 'NONE', ( #12691, #3895, #19367, #16632 ) ) ;
#1271=AXIS2_PLACEMENT_3D ( 'NONE', #2495, #2949, #11100 ) ;
#1285=DIRECTION ( 'NONE',  ( 1.224646799147353207E-16, 0.000000000000000000, 1.000000000000000000 ) ) ;
#1315=DIRECTION ( 'NONE',  ( -5.192538640813645496E-17, 1.000000000000000000, 6.359025825921378559E-33 ) ) ;
#1329=CARTESIAN_POINT ( 'NONE',  ( -9.718906393579157310, 43.49585613540820361, 70.88527860057354246 ) ) ;
#1351=EDGE_LOOP ( 'NONE', ( #16475, #826, #15426, #17574 ) ) ;
#1381=EDGE_LOOP ( 'NONE', ( #13518, #9293, #4886, #7780, #1024 ) ) ;
#1388=LINE ( 'NONE', #13685, #15292 ) ;
#1394=PLANE ( 'NONE',  #5062 ) ;
#1420=DIRECTION ( 'NONE',  ( -1.224646799147353207E-16, -0.000000000000000000, -1.000000000000000000 ) ) ;
#1527=VERTEX_POINT ( 'NONE', #18221 ) ;
#1562=ORIENTED_EDGE ( 'NONE', *, *, #20368, .T. ) ;
#1597=VECTOR ( 'NONE', #3258, 1000.000000000000000 ) ;
#1618=CARTESIAN_POINT ( 'NONE',  ( -8.638906393579159015, 41.58710221366784054, 69.00503344894293889 ) ) ;
#1619=CARTESIAN_POINT ( 'NONE',  ( -9.178906393579033818, 42.46645089659918426, 1067.751649863784678 ) ) ;
#1620=EDGE_LOOP ( 'NONE', ( #21323, #12891, #18593, #14003, #17914 ) ) ;
#1721=EDGE_LOOP ( 'NONE', ( #21799, #2456, #14260, #10433 ) ) ;
#1722=VECTOR ( 'NONE', #5893, 1000.000000000000000 ) ;
#1753=DIRECTION ( 'NONE',  ( 0.000000000000000000, 1.000000000000000000, -0.000000000000000000 ) ) ;
#1759=PLANE ( 'NONE',  #8228 ) ;
#1776=EDGE_LOOP ( 'NONE', ( #13596, #2910, #20139, #21929 ) ) ;
#1783=ORIENTED_EDGE ( 'NONE', *, *, #12823, .F. ) ;
#1809=EDGE_CURVE ( 'NONE', #10275, #10408, #8361, .T. ) ;
#1824=DIRECTION ( 'NONE',  ( -1.000000000000000000, -3.387630566026860322E-15, 1.224646799147353207E-16 ) ) ;
#1849=ORIENTED_EDGE ( 'NONE', *, *, #19303, .T. ) ;
#1857=DIRECTION ( 'NONE',  ( 1.000000000000000000, 0.000000000000000000, -1.224646799147353207E-16 ) ) ;
#1858=EDGE_CURVE ( 'NONE', #18170, #20955, #6345, .T. ) ;
#1878=CARTESIAN_POINT ( 'NONE',  ( -8.223741455913087250, 43.00645089659919051, 69.94509975324525897 ) ) ;
#1898=CARTESIAN_POINT ( 'NONE',  ( -8.134906293162368129, 43.00645089659919051, 68.06527860057354928 ) ) ;
#1906=MECHANICAL_DESIGN_GEOMETRIC_PRESENTATION_REPRESENTATION('',(#11918),#4057);
#1924=ORIENTED_EDGE ( 'NONE', *, *, #4283, .T. ) ;
#1948=CIRCLE ( 'NONE', #19460, 1.162443609680678280 ) ;
#1952=CARTESIAN_POINT ( 'NONE',  ( -8.638906393579159015, 44.91645089659918710, 70.88527860057354246 ) ) ;
#1959=CARTESIAN_POINT ( 'NONE',  ( -9.718906393579157310, 44.91645089659918710, 70.88527860057354246 ) ) ;
#1978=CARTESIAN_POINT ( 'NONE',  ( -6.678906393579161715, 42.46645089659918426, 61.53912392244307483 ) ) ;
#1994=UNCERTAINTY_MEASURE_WITH_UNIT (LENGTH_MEASURE( 1.000000000000000082E-05 ), #571, 'distance_accuracy_value', 'NONE');
#2022=AXIS2_PLACEMENT_3D ( 'NONE', #1213, #4596, #20044 ) ;
#2024=DIRECTION ( 'NONE',  ( -7.519041366722126991E-17, 0.4461977533474358326, -0.8949343913984425525 ) ) ;
#2032=CARTESIAN_POINT ( 'NONE',  ( -6.728906393579157097, 41.92645089659919933, 70.88527860057354246 ) ) ;
#2045=AXIS2_PLACEMENT_3D ( 'NONE', #6921, #20775, #1857 ) ;
#2070=AXIS2_PLACEMENT_3D ( 'NONE', #14269, #8918, #7577 ) ;
#2077=VECTOR ( 'NONE', #16297, 1000.000000000000000 ) ;
#2135=EDGE_LOOP ( 'NONE', ( #16925, #18666, #12516, #12086 ) ) ;
#2143=AXIS2_PLACEMENT_3D ( 'NONE', #19320, #84, #13824 ) ;
#2238=VERTEX_POINT ( 'NONE', #4400 ) ;
#2261=CARTESIAN_POINT ( 'NONE',  ( -9.178906393579158163, 42.46645089659918426, 68.06527860057354928 ) ) ;
#2341=ADVANCED_FACE ( 'NONE', ( #17894 ), #14529, .T. ) ;
#2371=ORIENTED_EDGE ( 'NONE', *, *, #7376, .T. ) ;
#2375=AXIS2_PLACEMENT_3D ( 'NONE', #5897, #19531, #4212 ) ;
#2388=ADVANCED_FACE ( 'NONE', ( #12852 ), #11499, .T. ) ;
#2403=DIRECTION ( 'NONE',  ( -1.224646799147353207E-16, -0.000000000000000000, -1.000000000000000000 ) ) ;
#2407=DIRECTION ( 'NONE',  ( 1.000000000000000000, 3.543406725251269872E-15, -1.224646799147353207E-16 ) ) ;
#2415=VECTOR ( 'NONE', #16537, 1000.000000000000000 ) ;
#2443=VECTOR ( 'NONE', #20678, 1000.000000000000000 ) ;
#2456=ORIENTED_EDGE ( 'NONE', *, *, #172, .T. ) ;
#2495=CARTESIAN_POINT ( 'NONE',  ( -9.178906393579033818, 42.46645089659918426, 1067.751649863784678 ) ) ;
#2534=FACE_OUTER_BOUND ( 'NONE', #5674, .T. ) ;
#2563=CARTESIAN_POINT ( 'NONE',  ( -8.378839169841056034, 43.00645089659919051, 68.06527860057354928 ) ) ;
#2594=CARTESIAN_POINT ( 'NONE',  ( -9.718906393579157310, 41.42245079618239600, 68.06527860057354928 ) ) ;
#2595=DIRECTION ( 'NONE',  ( -1.224646799147353207E-16, 0.000000000000000000, -1.000000000000000000 ) ) ;
#2639=DIRECTION ( 'NONE',  ( -1.000000000000000000, -3.387630566026860322E-15, 1.224646799147353207E-16 ) ) ;
#2662=LINE ( 'NONE', #9163, #8878 ) ;
#2694=ORIENTED_EDGE ( 'NONE', *, *, #7835, .F. ) ;
#2697=( LENGTH_UNIT ( ) NAMED_UNIT ( * ) SI_UNIT ( .MILLI., .METRE. ) );
#2714=FACE_OUTER_BOUND ( 'NONE', #14498, .T. ) ;
#2738=CARTESIAN_POINT ( 'NONE',  ( -8.149501154770145916, 43.00645089659919051, 70.88527860057354246 ) ) ;
#2761=ORIENTED_EDGE ( 'NONE', *, *, #9319, .F. ) ;
#2766=EDGE_LOOP ( 'NONE', ( #19772, #18008, #137, #4940 ) ) ;
#2797=AXIS2_PLACEMENT_3D ( 'NONE', #14005, #21082, #244 ) ;
#2809=CARTESIAN_POINT ( 'NONE',  ( -8.638906393579159015, 41.42245079618239600, 68.06527860057354928 ) ) ;
#2841=LINE ( 'NONE', #16233, #7885 ) ;
#2842=ADVANCED_FACE ( 'NONE', ( #2714 ), #16890, .F. ) ;
#2884=EDGE_LOOP ( 'NONE', ( #21358, #4109, #16987, #7689 ) ) ;
#2899=CARTESIAN_POINT ( 'NONE',  ( -9.978973617317260292, 41.92645089659918511, 68.06527860057354928 ) ) ;
#2907=ORIENTED_EDGE ( 'NONE', *, *, #18261, .F. ) ;
#2908=DIRECTION ( 'NONE',  ( 3.543406725251269872E-15, -1.000000000000000000, -5.100473277356134011E-17 ) ) ;
#2910=ORIENTED_EDGE ( 'NONE', *, *, #21503, .T. ) ;
#2949=DIRECTION ( 'NONE',  ( 1.224646799147353207E-16, 0.000000000000000000, 1.000000000000000000 ) ) ;
#2965=DIRECTION ( 'NONE',  ( 1.224646799147353207E-16, 0.000000000000000000, 1.000000000000000000 ) ) ;
#2975=CARTESIAN_POINT ( 'NONE',  ( -11.62890639357915923, 41.92645089659917801, 70.88527860057354246 ) ) ;
#3030=EDGE_CURVE ( 'NONE', #17645, #15161, #12200, .T. ) ;
#3067=DIRECTION ( 'NONE',  ( -1.000000000000000000, 0.000000000000000000, 1.224646799147353207E-16 ) ) ;
#3083=DIRECTION ( 'NONE',  ( 5.192538640813645496E-17, -1.000000000000000000, -6.359025825921378559E-33 ) ) ;
#3124=VECTOR ( 'NONE', #16804, 1000.000000000000114 ) ;
#3171=VERTEX_POINT ( 'NONE', #9414 ) ;
#3178=PLANE ( 'NONE',  #10786 ) ;
#3202=ORIENTED_EDGE ( 'NONE', *, *, #7717, .T. ) ;
#3258=DIRECTION ( 'NONE',  ( 1.224646799147353207E-16, 0.000000000000000000, 1.000000000000000000 ) ) ;
#3288=CARTESIAN_POINT ( 'NONE',  ( -8.134906293162361024, 41.92645089659918511, 68.06527860057354928 ) ) ;
#3325=EDGE_CURVE ( 'NONE', #9625, #1254, #20494, .T. ) ;
#3332=DIRECTION ( 'NONE',  ( -1.000000000000000000, 0.000000000000000000, 1.224646799147353207E-16 ) ) ;
#3352=LINE ( 'NONE', #6952, #7777 ) ;
#3353=DIRECTION ( 'NONE',  ( -1.224646799147353207E-16, 0.000000000000000000, -1.000000000000000000 ) ) ;
#3354=CARTESIAN_POINT ( 'NONE',  ( -8.638906393579159015, 43.49585613540820361, 70.88527860057354246 ) ) ;
#3380=CARTESIAN_POINT ( 'NONE',  ( -11.62890639357915923, 43.00645089659917630, 70.88527860057354246 ) ) ;
#3420=DIRECTION ( 'NONE',  ( -1.000000000000000000, -5.192538640813645496E-17, 7.145994714117440585E-17 ) ) ;
#3463=EDGE_CURVE ( 'NONE', #14452, #6925, #10416, .T. ) ;
#3570=CARTESIAN_POINT ( 'NONE',  ( -9.178906393579158163, 42.46645089659918426, 68.06527860057354928 ) ) ;
#3621=FACE_OUTER_BOUND ( 'NONE', #2135, .T. ) ;
#3647=EDGE_LOOP ( 'NONE', ( #19238, #7391, #2907, #1058 ) ) ;
#3651=VERTEX_POINT ( 'NONE', #14407 ) ;
#3677=CARTESIAN_POINT ( 'NONE',  ( -9.178906393579161715, 44.96645089659919137, 61.53912392244307483 ) ) ;
#3680=VERTEX_POINT ( 'NONE', #2563 ) ;
#3696=DIRECTION ( 'NONE',  ( -1.000000000000000000, 0.000000000000000000, 0.000000000000000000 ) ) ;
#3707=( GEOMETRIC_REPRESENTATION_CONTEXT ( 3 ) GLOBAL_UNCERTAINTY_ASSIGNED_CONTEXT ( ( #12276 ) ) GLOBAL_UNIT_ASSIGNED_CONTEXT ( ( #2697, #20958, #10986 ) ) REPRESENTATION_CONTEXT ( 'NONE', 'WORKASPACE' ) );
#3745=ADVANCED_FACE ( 'NONE', ( #11065 ), #16087, .T. ) ;
#3887=EDGE_LOOP ( 'NONE', ( #13715, #243, #12699, #7282 ) ) ;
#3895=ORIENTED_EDGE ( 'NONE', *, *, #10755, .F. ) ;
#3899=CARTESIAN_POINT ( 'NONE',  ( -9.178906393579158163, 42.46645089659918426, 70.88527860057354246 ) ) ;
#3902=CARTESIAN_POINT ( 'NONE',  ( -8.149501154770145916, 43.00645089659919051, 70.88527860057354246 ) ) ;
#3937=ORIENTED_EDGE ( 'NONE', *, *, #14119, .F. ) ;
#3965=VERTEX_POINT ( 'NONE', #1978 ) ;
#4009=( NAMED_UNIT ( * ) SI_UNIT ( $, .STERADIAN. ) SOLID_ANGLE_UNIT ( ) );
#4015=ORIENTED_EDGE ( 'NONE', *, *, #4115, .T. ) ;
#4025=VECTOR ( 'NONE', #20915, 1000.000000000000227 ) ;
#4057=( GEOMETRIC_REPRESENTATION_CONTEXT ( 3 ) GLOBAL_UNCERTAINTY_ASSIGNED_CONTEXT ( ( #1994 ) ) GLOBAL_UNIT_ASSIGNED_CONTEXT ( ( #571, #12757, #14230 ) ) REPRESENTATION_CONTEXT ( 'NONE', 'WORKASPACE' ) );
#4060=CARTESIAN_POINT ( 'NONE',  ( -11.62890639357915923, 43.00645089659917630, 70.88527860057354246 ) ) ;
#4067=ORIENTED_EDGE ( 'NONE', *, *, #19613, .T. ) ;
#4084=PLANE ( 'NONE',  #22127 ) ;
#4087=CYLINDRICAL_SURFACE ( 'NONE', #14197, 2.500000000000000444 ) ;
#4105=VECTOR ( 'NONE', #5415, 1000.000000000000114 ) ;
#4109=ORIENTED_EDGE ( 'NONE', *, *, #983, .F. ) ;
#4115=EDGE_CURVE ( 'NONE', #8087, #538, #6730, .T. ) ;
#4144=ORIENTED_EDGE ( 'NONE', *, *, #18101, .F. ) ;
#4147=ORIENTED_EDGE ( 'NONE', *, *, #8333, .F. ) ;
#4202=CARTESIAN_POINT ( 'NONE',  ( -11.67890639357916172, 42.46645089659918426, 61.53912392244307483 ) ) ;
#4205=ADVANCED_FACE ( 'NONE', ( #5965 ), #20554, .F. ) ;
#4212=DIRECTION ( 'NONE',  ( -1.000000000000000000, 0.000000000000000000, 0.000000000000000000 ) ) ;
#4236=EDGE_LOOP ( 'NONE', ( #10803, #8417, #14392, #7189 ) ) ;
#4251=PRODUCT_DEFINITION ( 'UNKNOWN', '', #11935, #18704 ) ;
#4279=CARTESIAN_POINT ( 'NONE',  ( -8.638906393579159015, 43.26651812033729527, 68.06527860057354928 ) ) ;
#4280=ORIENTED_EDGE ( 'NONE', *, *, #1060, .F. ) ;
#4283=EDGE_CURVE ( 'NONE', #8087, #11459, #16072, .T. ) ;
#4356=ORIENTED_EDGE ( 'NONE', *, *, #9644, .T. ) ;
#4362=ORIENTED_EDGE ( 'NONE', *, *, #4743, .T. ) ;
#4367=ORIENTED_EDGE ( 'NONE', *, *, #4785, .F. ) ;
#4372=LINE ( 'NONE', #6995, #15021 ) ;
#4400=CARTESIAN_POINT ( 'NONE',  ( -6.728906393579157097, 41.92645089659919933, 70.88527860057354246 ) ) ;
#4405=DIRECTION ( 'NONE',  ( -1.224646799147353207E-16, -0.000000000000000000, -1.000000000000000000 ) ) ;
#4452=EDGE_CURVE ( 'NONE', #12093, #7942, #16458, .T. ) ;
#4494=AXIS2_PLACEMENT_3D ( 'NONE', #8367, #11929, #8710 ) ;
#4506=DIRECTION ( 'NONE',  ( 0.000000000000000000, 1.000000000000000000, 0.000000000000000000 ) ) ;
#4596=DIRECTION ( 'NONE',  ( -1.224646799147353207E-16, -0.000000000000000000, -1.000000000000000000 ) ) ;
#4603=AXIS2_PLACEMENT_3D ( 'NONE', #2261, #7210, #20750 ) ;
#4624=EDGE_CURVE ( 'NONE', #14279, #21390, #10152, .T. ) ;
#4649=CIRCLE ( 'NONE', #11426, 1.250000000000001110 ) ;
#4652=CARTESIAN_POINT ( 'NONE',  ( -6.678906393579158163, 42.46645089659918426, 74.06027860057353962 ) ) ;
#4743=EDGE_CURVE ( 'NONE', #3965, #412, #9961, .T. ) ;
#4774=FACE_OUTER_BOUND ( 'NONE', #2766, .T. ) ;
#4785=EDGE_CURVE ( 'NONE', #21235, #3651, #12580, .T. ) ;
#4838=LINE ( 'NONE', #9993, #3124 ) ;
#4863=VECTOR ( 'NONE', #1315, 1000.000000000000000 ) ;
#4876=DIRECTION ( 'NONE',  ( 1.224646799147353207E-16, 0.000000000000000000, 1.000000000000000000 ) ) ;
#4885=VECTOR ( 'NONE', #16994, 1000.000000000000227 ) ;
#4886=ORIENTED_EDGE ( 'NONE', *, *, #11565, .T. ) ;
#4892=EDGE_CURVE ( 'NONE', #1527, #12093, #14597, .T. ) ;
#4934=DIRECTION ( 'NONE',  ( -4.078297354714382145E-17, -0.4461977533474358326, -0.8949343913984425525 ) ) ;
#4940=ORIENTED_EDGE ( 'NONE', *, *, #7389, .F. ) ;
#4995=CARTESIAN_POINT ( 'NONE',  ( -8.638906393579159015, 41.51128595893310802, 69.94509975324525897 ) ) ;
#5044=LINE ( 'NONE', #8731, #7946 ) ;
#5062=AXIS2_PLACEMENT_3D ( 'NONE', #20201, #16400, #6464 ) ;
#5069=LINE ( 'NONE', #3380, #13461 ) ;
#5099=CARTESIAN_POINT ( 'NONE',  ( -11.67890639357915816, 42.46645089659918426, 74.06027860057353962 ) ) ;
#5160=DIRECTION ( 'NONE',  ( -1.000000000000000000, 0.000000000000000000, 0.000000000000000000 ) ) ;
#5165=VECTOR ( 'NONE', #4934, 1000.000000000000114 ) ;
#5215=AXIS2_PLACEMENT_3D ( 'NONE', #5904, #16948, #11909 ) ;
#5222=EDGE_LOOP ( 'NONE', ( #8586, #14321, #2761, #9094, #21705, #12029, #8332 ) ) ;
#5313=EDGE_CURVE ( 'NONE', #21235, #16141, #13204, .T. ) ;
#5345=ORIENTED_EDGE ( 'NONE', *, *, #15088, .F. ) ;
#5359=CARTESIAN_POINT ( 'NONE',  ( -9.718906393579157310, 41.42245079618239600, 68.06527860057354928 ) ) ;
#5397=PRODUCT_CONTEXT ( 'NONE', #19880, 'mechanical' ) ;
#5415=DIRECTION ( 'NONE',  ( -0.4461977533474358326, -1.454668808886070861E-15, -0.8949343913984425525 ) ) ;
#5455=EDGE_CURVE ( 'NONE', #11459, #3680, #19906, .T. ) ;
#5461=ORIENTED_EDGE ( 'NONE', *, *, #12546, .T. ) ;
#5472=CIRCLE ( 'NONE', #14011, 4.575000000000001066 ) ;
#5579=SURFACE_SIDE_STYLE ('',( #8818 ) ) ;
#5656=PLANE ( 'NONE',  #16368 ) ;
#5674=EDGE_LOOP ( 'NONE', ( #13232, #5345, #6578, #4147 ) ) ;
#5691=CARTESIAN_POINT ( 'NONE',  ( -9.718906393579157310, 44.91645089659918710, 70.88527860057354246 ) ) ;
#5827=DIRECTION ( 'NONE',  ( 1.224646799147353207E-16, 0.000000000000000000, 1.000000000000000000 ) ) ;
#5878=CARTESIAN_POINT ( 'NONE',  ( -9.178906393579158163, 42.46645089659918426, 70.38908280829822672 ) ) ;
#5885=DIRECTION ( 'NONE',  ( 0.4461977533474358326, 1.557891129246303114E-15, 0.8949343913984425525 ) ) ;
#5890=PLANE ( 'NONE',  #13968 ) ;
#5893=DIRECTION ( 'NONE',  ( -1.327594496921025717E-16, -1.000000000000000000, 1.625834351219974904E-32 ) ) ;
#5897=CARTESIAN_POINT ( 'NONE',  ( -9.178906393579158163, 42.46645089659918426, 70.88527860057354246 ) ) ;
#5904=CARTESIAN_POINT ( 'NONE',  ( -9.178906393579158163, 42.46645089659918426, 68.75385983073485363 ) ) ;
#5918=ADVANCED_FACE ( 'NONE', ( #8612 ), #10190, .F. ) ;
#5922=CARTESIAN_POINT ( 'NONE',  ( -9.978973617317260292, 41.92645089659918511, 68.06527860057354928 ) ) ;
#5924=CARTESIAN_POINT ( 'NONE',  ( -9.178906393579158163, 42.46645089659918426, 68.06527860057354928 ) ) ;
#5955=EDGE_CURVE ( 'NONE', #16035, #18107, #11962, .T. ) ;
#5965=FACE_OUTER_BOUND ( 'NONE', #1381, .T. ) ;
#5987=MANIFOLD_SOLID_BREP ( 'Stock-MAS-696-1', #10645 ) ;
#6004=VECTOR ( 'NONE', #14778, 1000.000000000000000 ) ;
#6065=EDGE_CURVE ( 'NONE', #3680, #538, #9482, .T. ) ;
#6080=ADVANCED_FACE ( 'NONE', ( #13834 ), #20691, .T. ) ;
#6082=DIRECTION ( 'NONE',  ( -1.000000000000000000, -3.543406725251269872E-15, 1.224646799147353207E-16 ) ) ;
#6130=CARTESIAN_POINT ( 'NONE',  ( -8.213656393579155335, 42.46645089659918426, 68.06527860057354928 ) ) ;
#6161=ORIENTED_EDGE ( 'NONE', *, *, #9644, .F. ) ;
#6178=CARTESIAN_POINT ( 'NONE',  ( -9.978973617317267397, 43.00645089659918341, 68.06527860057354928 ) ) ;
#6188=VECTOR ( 'NONE', #13365, 1000.000000000000000 ) ;
#6211=CARTESIAN_POINT ( 'NONE',  ( -10.22290649399594642, 41.92645089659918511, 68.06527860057354928 ) ) ;
#6233=AXIS2_PLACEMENT_3D ( 'NONE', #3899, #15733, #19427 ) ;
#6297=VECTOR ( 'NONE', #20281, 1000.000000000000000 ) ;
#6334=LINE ( 'NONE', #4652, #17902 ) ;
#6345=LINE ( 'NONE', #14479, #16195 ) ;
#6348=AXIS2_PLACEMENT_3D ( 'NONE', #8062, #7853, #19933 ) ;
#6369=AXIS2_PLACEMENT_3D ( 'NONE', #14755, #2908, #8173 ) ;
#6429=VECTOR ( 'NONE', #7064, 999.9999999999998863 ) ;
#6454=PRODUCT ( 'Cross Recess Screw', 'Cross Recess Screw', '', ( #5397 ) ) ;
#6464=DIRECTION ( 'NONE',  ( 1.000000000000000000, 0.000000000000000000, -1.224646799147353207E-16 ) ) ;
#6517=EDGE_CURVE ( 'NONE', #10408, #10275, #1255, .T. ) ;
#6521=DIRECTION ( 'NONE',  ( -1.224646799147353207E-16, -0.000000000000000000, -1.000000000000000000 ) ) ;
#6528=ORIENTED_EDGE ( 'NONE', *, *, #21307, .F. ) ;
#6530=AXIS2_PLACEMENT_3D ( 'NONE', #16099, #1113, #13074 ) ;
#6578=ORIENTED_EDGE ( 'NONE', *, *, #3030, .T. ) ;
#6579=CARTESIAN_POINT ( 'NONE',  ( -8.638906393579159015, 41.43704565779017202, 70.88527860057354246 ) ) ;
#6663=ORIENTED_EDGE ( 'NONE', *, *, #14980, .F. ) ;
#6678=ORIENTED_EDGE ( 'NONE', *, *, #22130, .T. ) ;
#6730=CIRCLE ( 'NONE', #13493, 1.162443609680678280 ) ;
#6733=DIRECTION ( 'NONE',  ( -1.038507728162729346E-16, -1.000000000000000000, 1.271805165184275985E-32 ) ) ;
#6818=EDGE_CURVE ( 'NONE', #12110, #7942, #7201, .T. ) ;
#6822=CARTESIAN_POINT ( 'NONE',  ( -9.178906393579158163, 42.46645089659918426, 67.85468508031152624 ) ) ;
#6825=PLANE ( 'NONE',  #16146 ) ;
#6827=CARTESIAN_POINT ( 'NONE',  ( -9.178906393579158163, 42.46645089659918426, 74.06027860057353962 ) ) ;
#6834=EDGE_CURVE ( 'NONE', #21631, #3171, #1948, .T. ) ;
#6837=ORIENTED_EDGE ( 'NONE', *, *, #1809, .F. ) ;
#6841=CARTESIAN_POINT ( 'NONE',  ( -9.718906393579157310, 40.01645089659919563, 70.88527860057354246 ) ) ;
#6842=ADVANCED_FACE ( 'NONE', ( #12533 ), #14332, .T. ) ;
#6921=CARTESIAN_POINT ( 'NONE',  ( -8.638906393579159015, 43.51045099701597252, 68.06527860057354928 ) ) ;
#6925=VERTEX_POINT ( 'NONE', #7637 ) ;
#6950=DIRECTION ( 'NONE',  ( 1.224646799147353207E-16, 0.000000000000000000, 1.000000000000000000 ) ) ;
#6952=CARTESIAN_POINT ( 'NONE',  ( -9.718906393579157310, 43.51045099701597252, 68.06527860057354928 ) ) ;
#6995=CARTESIAN_POINT ( 'NONE',  ( -9.178906393579158163, 42.46645089659918426, 67.75164986378473486 ) ) ;
#6996=EDGE_CURVE ( 'NONE', #299, #10408, #16785, .T. ) ;
#7020=CARTESIAN_POINT ( 'NONE',  ( -4.603906393579157097, 42.46645089659918426, 70.88527860057354246 ) ) ;
#7050=EDGE_CURVE ( 'NONE', #22112, #18107, #12058, .T. ) ;
#7064=DIRECTION ( 'NONE',  ( 0.7193398003386525241, -8.809371839840268653E-17, 0.6946583704589959218 ) ) ;
#7073=ORIENTED_EDGE ( 'NONE', *, *, #19525, .T. ) ;
#7087=DIRECTION ( 'NONE',  ( -1.000000000000000000, -3.491481338843133355E-15, 1.224646799147353207E-16 ) ) ;
#7164=VECTOR ( 'NONE', #3332, 1000.000000000000000 ) ;
#7182=ORIENTED_EDGE ( 'NONE', *, *, #17279, .T. ) ;
#7189=ORIENTED_EDGE ( 'NONE', *, *, #14119, .T. ) ;
#7201=LINE ( 'NONE', #20741, #4105 ) ;
#7210=DIRECTION ( 'NONE',  ( 1.224646799147353207E-16, 0.000000000000000000, 1.000000000000000000 ) ) ;
#7251=ORIENTED_EDGE ( 'NONE', *, *, #8939, .T. ) ;
#7272=ADVANCED_BREP_SHAPE_REPRESENTATION ( '', ( #5987, #17493 ), #3707 ) ;
#7282=ORIENTED_EDGE ( 'NONE', *, *, #14980, .T. ) ;
#7306=CARTESIAN_POINT ( 'NONE',  ( -10.20831163238817574, 43.00645089659918341, 70.88527860057354246 ) ) ;
#7313=SURFACE_STYLE_FILL_AREA ( #9315 ) ;
#7376=EDGE_CURVE ( 'NONE', #17182, #14452, #190, .T. ) ;
#7382=CARTESIAN_POINT ( 'NONE',  ( -11.62890639357915923, 41.92645089659917801, 70.88527860057354246 ) ) ;
#7389=EDGE_CURVE ( 'NONE', #20601, #3171, #7803, .T. ) ;
#7391=ORIENTED_EDGE ( 'NONE', *, *, #12503, .T. ) ;
#7393=AXIS2_PLACEMENT_3D ( 'NONE', #496, #6950, #105 ) ;
#7431=CIRCLE ( 'NONE', #18866, 0.9652499999999990532 ) ;
#7492=ADVANCED_FACE ( 'NONE', ( #4774 ), #18747, .T. ) ;
#7577=DIRECTION ( 'NONE',  ( -1.000000000000000000, 0.000000000000000000, 0.000000000000000000 ) ) ;
#7637=CARTESIAN_POINT ( 'NONE',  ( -4.603906393579157097, 42.46645089659918426, 70.38908280829822672 ) ) ;
#7689=ORIENTED_EDGE ( 'NONE', *, *, #11853, .T. ) ;
#7717=EDGE_CURVE ( 'NONE', #6925, #299, #19866, .T. ) ;
#7777=VECTOR ( 'NONE', #6733, 1000.000000000000000 ) ;
#7780=ORIENTED_EDGE ( 'NONE', *, *, #10755, .T. ) ;
#7803=B_SPLINE_CURVE_WITH_KNOTS ( 'NONE', 3,
 ( #65, #1618, #4995, #6579 ),
 .UNSPECIFIED., .F., .F.,
 ( 4, 4 ),
 ( 0.005071647684206891972, 0.007900577432593609145 ),
 .UNSPECIFIED. ) ;
#7807=LINE ( 'NONE', #21571, #11829 ) ;
#7835=EDGE_CURVE ( 'NONE', #412, #3965, #20220, .T. ) ;
#7853=DIRECTION ( 'NONE',  ( 1.224646799147353207E-16, 0.000000000000000000, 1.000000000000000000 ) ) ;
#7854=AXIS2_PLACEMENT_3D ( 'NONE', #10415, #11956, #8391 ) ;
#7885=VECTOR ( 'NONE', #4506, 1000.000000000000000 ) ;
#7942=VERTEX_POINT ( 'NONE', #18122 ) ;
#7946=VECTOR ( 'NONE', #22055, 1000.000000000000000 ) ;
#7954=ORIENTED_EDGE ( 'NONE', *, *, #6996, .T. ) ;
#7962=CARTESIAN_POINT ( 'NONE',  ( -8.638906393579159015, 40.01645089659919563, 70.88527860057354246 ) ) ;
#8001=ORIENTED_EDGE ( 'NONE', *, *, #7389, .T. ) ;
#8062=CARTESIAN_POINT ( 'NONE',  ( -9.178906393579158163, 42.46645089659918426, 70.38908280829822672 ) ) ;
#8067=CARTESIAN_POINT ( 'NONE',  ( -9.718906393579157310, 41.43704565779017202, 70.88527860057354246 ) ) ;
#8068=AXIS2_PLACEMENT_3D ( 'NONE', #18404, #3420, #3083 ) ;
#8087=VERTEX_POINT ( 'NONE', #3354 ) ;
#8092=ORIENTED_EDGE ( 'NONE', *, *, #6834, .T. ) ;
#8128=AXIS2_PLACEMENT_3D ( 'NONE', #14443, #1031, #18030 ) ;
#8157=CARTESIAN_POINT ( 'NONE',  ( -6.728906393579160650, 43.00645089659919762, 70.88527860057354246 ) ) ;
#8173=DIRECTION ( 'NONE',  ( 1.000000000000000000, 3.543406725251269872E-15, -1.224646799147353207E-16 ) ) ;
#8183=FACE_OUTER_BOUND ( 'NONE', #4236, .T. ) ;
#8202=CARTESIAN_POINT ( 'NONE',  ( -11.62890639357915923, 41.92645089659917801, 70.88527860057354246 ) ) ;
#8228=AXIS2_PLACEMENT_3D ( 'NONE', #15405, #12030, #18879 ) ;
#8231=CARTESIAN_POINT ( 'NONE',  ( -8.149501154770138811, 41.92645089659918511, 70.88527860057354246 ) ) ;
#8318=AXIS2_PLACEMENT_3D ( 'NONE', #15584, #4876, #11685 ) ;
#8322=CARTESIAN_POINT ( 'NONE',  ( -9.718906393579157310, 41.66638367286108746, 68.06527860057354928 ) ) ;
#8332=ORIENTED_EDGE ( 'NONE', *, *, #10323, .F. ) ;
#8333=EDGE_CURVE ( 'NONE', #15347, #15161, #8598, .T. ) ;
#8361=CIRCLE ( 'NONE', #6233, 4.575000000000001066 ) ;
#8367=CARTESIAN_POINT ( 'NONE',  ( -9.178906393579158163, 42.46645089659918426, 67.85468508031152624 ) ) ;
#8371=CARTESIAN_POINT ( 'NONE',  ( -9.718906393579157310, 41.42245079618239600, 68.06527860057354928 ) ) ;
#8391=DIRECTION ( 'NONE',  ( -1.000000000000000000, 0.000000000000000000, 0.000000000000000000 ) ) ;
#8411=STYLED_ITEM ( 'NONE', ( #10398 ), #5987 ) ;
#8417=ORIENTED_EDGE ( 'NONE', *, *, #7376, .F. ) ;
#8584=FACE_OUTER_BOUND ( 'NONE', #5222, .T. ) ;
#8586=ORIENTED_EDGE ( 'NONE', *, *, #14136, .F. ) ;
#8598=B_SPLINE_CURVE_WITH_KNOTS ( 'NONE', 3,
 ( #5922, #16186, #11163, #1096 ),
 .UNSPECIFIED., .F., .F.,
 ( 4, 4 ),
 ( 0.005071647684206891105, 0.007900577432593609145 ),
 .UNSPECIFIED. ) ;
#8612=FACE_OUTER_BOUND ( 'NONE', #19198, .T. ) ;
#8647=AXIS2_PLACEMENT_3D ( 'NONE', #14798, #20177, #14579 ) ;
#8663=AXIS2_PLACEMENT_3D ( 'NONE', #9404, #14420, #21272 ) ;
#8666=ORIENTED_EDGE ( 'NONE', *, *, #6517, .F. ) ;
#8710=DIRECTION ( 'NONE',  ( -1.000000000000000000, 0.000000000000000000, 0.000000000000000000 ) ) ;
#8731=CARTESIAN_POINT ( 'NONE',  ( -6.728906393579157097, 41.92645089659919933, 70.88527860057354246 ) ) ;
#8771=COLOUR_RGB ( '', 0.66274510, 0.83137255, 0.94901961) ;
#8781=CYLINDRICAL_SURFACE ( 'NONE', #8318, 4.575000000000001066 ) ;
#8785=CIRCLE ( 'NONE', #4494, 2.500000000000000444 ) ;
#8797=VECTOR ( 'NONE', #17103, 1000.000000000000000 ) ;
#8818=SURFACE_STYLE_FILL_AREA ( #12156 ) ;
#8847=EDGE_CURVE ( 'NONE', #21631, #1527, #1036, .T. ) ;
#8878=VECTOR ( 'NONE', #2024, 1000.000000000000114 ) ;
#8881=CARTESIAN_POINT ( 'NONE',  ( -9.718906393579157310, 43.26651812033729527, 68.06527860057354928 ) ) ;
#8918=DIRECTION ( 'NONE',  ( -1.224646799147353207E-16, -0.000000000000000000, -1.000000000000000000 ) ) ;
#8939=EDGE_CURVE ( 'NONE', #412, #9924, #18396, .T. ) ;
#8978=CARTESIAN_POINT ( 'NONE',  ( -11.62890639357915923, 41.92645089659917801, 70.88527860057354246 ) ) ;
#9001=CARTESIAN_POINT ( 'NONE',  ( -10.14415639357916099, 42.46645089659918426, 68.06527860057354928 ) ) ;
#9020=DIRECTION ( 'NONE',  ( -1.224646799147353207E-16, -0.000000000000000000, -1.000000000000000000 ) ) ;
#9024=DIRECTION ( 'NONE',  ( 1.224646799147353207E-16, 0.000000000000000000, 1.000000000000000000 ) ) ;
#9044=EDGE_LOOP ( 'NONE', ( #11330, #2694, #7251, #6528 ) ) ;
#9090=FILL_AREA_STYLE_COLOUR ( '', #10853 ) ;
#9094=ORIENTED_EDGE ( 'NONE', *, *, #13987, .F. ) ;
#9155=APPLICATION_CONTEXT ( 'automotive_design' ) ;
#9163=CARTESIAN_POINT ( 'NONE',  ( -9.718906393579157310, 40.01645089659919563, 70.88527860057354246 ) ) ;
#9168=EDGE_CURVE ( 'NONE', #14279, #13526, #10413, .T. ) ;
#9237=DIRECTION ( 'NONE',  ( -1.000000000000000000, 0.000000000000000000, 0.000000000000000000 ) ) ;
#9252=DIRECTION ( 'NONE',  ( -6.375533427066372209E-18, 0.4461977533474357216, -0.8949343913984425525 ) ) ;
#9293=ORIENTED_EDGE ( 'NONE', *, *, #5955, .T. ) ;
#9315=FILL_AREA_STYLE ('',( #9090 ) ) ;
#9319=EDGE_CURVE ( 'NONE', #15347, #16035, #14992, .T. ) ;
#9404=CARTESIAN_POINT ( 'NONE',  ( -9.178906393579158163, 42.46645089659918426, 70.38908280829822672 ) ) ;
#9414=CARTESIAN_POINT ( 'NONE',  ( -8.638906393579159015, 41.43704565779017202, 70.88527860057354246 ) ) ;
#9419=CARTESIAN_POINT ( 'NONE',  ( -8.638906393579159015, 43.51045099701597252, 68.06527860057354928 ) ) ;
#9427=EDGE_CURVE ( 'NONE', #1527, #20601, #20724, .T. ) ;
#9433=CARTESIAN_POINT ( 'NONE',  ( -9.718906393579157310, 43.51045099701597962, 68.06527860057354928 ) ) ;
#9482=B_SPLINE_CURVE_WITH_KNOTS ( 'NONE', 3,
 ( #19430, #15514, #1878, #3902 ),
 .UNSPECIFIED., .F., .F.,
 ( 4, 4 ),
 ( 0.005071647684206891105, 0.007900577432593609145 ),
 .UNSPECIFIED. ) ;
#9488=CARTESIAN_POINT ( 'NONE',  ( -9.718906393579157310, 43.51045099701597252, 68.06527860057354928 ) ) ;
#9504=EDGE_CURVE ( 'NONE', #17182, #9924, #4649, .T. ) ;
#9530=CARTESIAN_POINT ( 'NONE',  ( -8.134906293162361024, 41.92645089659918511, 68.06527860057354928 ) ) ;
#9549=DIRECTION ( 'NONE',  ( -1.000000000000000000, 0.000000000000000000, 0.000000000000000000 ) ) ;
#9625=VERTEX_POINT ( 'NONE', #1952 ) ;
#9632=ORIENTED_EDGE ( 'NONE', *, *, #15442, .T. ) ;
#9644=EDGE_CURVE ( 'NONE', #14279, #15161, #17146, .T. ) ;
#9677=DIRECTION ( 'NONE',  ( -1.000000000000000000, 0.000000000000000000, 0.000000000000000000 ) ) ;
#9696=EDGE_LOOP ( 'NONE', ( #14415, #3937, #7954, #18380 ) ) ;
#9723=CARTESIAN_POINT ( 'NONE',  ( -9.178906393579158163, 42.46645089659918426, 68.06527860057354928 ) ) ;
#9763=PLANE ( 'NONE',  #274 ) ;
#9767=CARTESIAN_POINT ( 'NONE',  ( 0.000000000000000000, 0.000000000000000000, 0.000000000000000000 ) ) ;
#9790=ADVANCED_FACE ( 'NONE', ( #11340 ), #4084, .T. ) ;
#9835=LINE ( 'NONE', #16638, #4863 ) ;
#9843=MECHANICAL_DESIGN_GEOMETRIC_PRESENTATION_REPRESENTATION('',(#8411),#19473);
#9879=VECTOR ( 'NONE', #7087, 1000.000000000000000 ) ;
#9888=VECTOR ( 'NONE', #6082, 1000.000000000000000 ) ;
#9921=ORIENTED_EDGE ( 'NONE', *, *, #20368, .F. ) ;
#9924=VERTEX_POINT ( 'NONE', #11780 ) ;
#9930=ORIENTED_EDGE ( 'NONE', *, *, #14662, .F. ) ;
#9961=CIRCLE ( 'NONE', #2070, 2.500000000000000444 ) ;
#9993=CARTESIAN_POINT ( 'NONE',  ( -13.75390639357915923, 42.46645089659918426, 70.38908280829822672 ) ) ;
#10054=LINE ( 'NONE', #22027, #7164 ) ;
#10074=ADVANCED_FACE ( 'NONE', ( #15894 ), #12043, .F. ) ;
#10088=CARTESIAN_POINT ( 'NONE',  ( -10.20831163238817574, 43.00645089659918341, 70.88527860057354246 ) ) ;
#10108=ORIENTED_EDGE ( 'NONE', *, *, #15287, .F. ) ;
#10113=VECTOR ( 'NONE', #19052, 1000.000000000000000 ) ;
#10138=DIRECTION ( 'NONE',  ( -1.000000000000000000, 0.000000000000000000, 1.442933311647907116E-16 ) ) ;
#10152=LINE ( 'NONE', #1959, #2443 ) ;
#10165=LINE ( 'NONE', #13399, #8797 ) ;
#10190=CONICAL_SURFACE ( 'NONE', #21639, 0.9652499999999990532, 0.06981317007976590994 ) ;
#10217=CARTESIAN_POINT ( 'NONE',  ( -9.178906393579158163, 42.46645089659918426, 68.06527860057354928 ) ) ;
#10226=CARTESIAN_POINT ( 'NONE',  ( -12.06058343050541204, 42.46645089659918426, 68.75385983073485363 ) ) ;
#10262=EDGE_LOOP ( 'NONE', ( #16732, #16149, #10108, #11963, #4367, #11604, #9921, #4015, #16028, #6663, #14727, #8092, #4280, #15412, #18359, #4356 ) ) ;
#10271=VECTOR ( 'NONE', #15320, 1000.000000000000000 ) ;
#10274=FACE_OUTER_BOUND ( 'NONE', #3647, .T. ) ;
#10275=VERTEX_POINT ( 'NONE', #7020 ) ;
#10302=B_SPLINE_CURVE_WITH_KNOTS ( 'NONE', 3,
 ( #18341, #16652, #13411, #1329 ),
 .UNSPECIFIED., .F., .F.,
 ( 4, 4 ),
 ( 0.005071647684206891972, 0.007900577432593609145 ),
 .UNSPECIFIED. ) ;
#10323=EDGE_CURVE ( 'NONE', #12999, #1527, #7431, .T. ) ;
#10386=DIRECTION ( 'NONE',  ( 0.000000000000000000, 1.000000000000000000, 0.000000000000000000 ) ) ;
#10387=CARTESIAN_POINT ( 'NONE',  ( -10.22290649399594997, 43.00645089659918341, 68.06527860057354928 ) ) ;
#10390=ADVANCED_FACE ( 'NONE', ( #13930 ), #4087, .T. ) ;
#10395=PRODUCT_DEFINITION_SHAPE ( 'NONE', 'NONE',  #4251 ) ;
#10398=PRESENTATION_STYLE_ASSIGNMENT (( #21132 ) ) ;
#10408=VERTEX_POINT ( 'NONE', #19091 ) ;
#10413=B_SPLINE_CURVE_WITH_KNOTS ( 'NONE', 3,
 ( #8067, #19941, #1118, #21731 ),
 .UNSPECIFIED., .F., .F.,
 ( 4, 4 ),
 ( 0.001759598111914162421, 0.004588913574811922039 ),
 .UNSPECIFIED. ) ;
#10415=CARTESIAN_POINT ( 'NONE',  ( -9.178906393579158163, 42.46645089659918426, 68.06527860057354928 ) ) ;
#10416=LINE ( 'NONE', #208, #6429 ) ;
#10433=ORIENTED_EDGE ( 'NONE', *, *, #7050, .T. ) ;
#10477=CARTESIAN_POINT ( 'NONE',  ( -8.638906393579159015, 43.34579957953053508, 69.00503344894293889 ) ) ;
#10496=DIRECTION ( 'NONE',  ( -1.224646799147353207E-16, 0.000000000000000000, -1.000000000000000000 ) ) ;
#10512=FACE_OUTER_BOUND ( 'NONE', #1620, .T. ) ;
#10545=DIRECTION ( 'NONE',  ( 1.000000000000000000, 3.387630566026860322E-15, -1.224646799147353207E-16 ) ) ;
#10582=ADVANCED_FACE ( 'NONE', ( #11891 ), #22035, .F. ) ;
#10626=DIRECTION ( 'NONE',  ( -1.000000000000000000, 0.000000000000000000, 0.000000000000000000 ) ) ;
#10629=CARTESIAN_POINT ( 'NONE',  ( -9.178906393579158163, 42.46645089659918426, 67.75164986378473486 ) ) ;
#10645=CLOSED_SHELL ( 'NONE', ( #16063, #18600, #10390, #2388, #19742, #15420, #6842, #7492, #17490, #13006, #4205, #16248, #21264, #14822, #21904, #11810, #19130, #13194, #18146, #448, #6080, #10582, #14986, #2341, #21233, #9790, #3745, #10074, #12525, #2842, #5918, #11107 ) ) ;
#10698=CARTESIAN_POINT ( 'NONE',  ( -8.638906393579159015, 43.49585613540820361, 70.88527860057354246 ) ) ;
#10755=EDGE_CURVE ( 'NONE', #15401, #14671, #10165, .T. ) ;
#10780=EDGE_LOOP ( 'NONE', ( #494, #11885, #7073, #18153 ) ) ;
#10786=AXIS2_PLACEMENT_3D ( 'NONE', #3288, #13454, #1824 ) ;
#10803=ORIENTED_EDGE ( 'NONE', *, *, #3463, .F. ) ;
#10827=EDGE_CURVE ( 'NONE', #11459, #1254, #9835, .T. ) ;
#10840=SHAPE_REPRESENTATION ( 'Cross Recess Screw', ( #17493 ), #3707 ) ;
#10848=EDGE_LOOP ( 'NONE', ( #12685, #13126, #13149, #15961 ) ) ;
#10853=COLOUR_RGB ( '', 0.66274510, 0.83137255, 0.94901961) ;
#10970=CARTESIAN_POINT ( 'NONE',  ( -9.178906393579161715, 42.46645089659918426, 61.53912392244307483 ) ) ;
#10986=( NAMED_UNIT ( * ) SI_UNIT ( $, .STERADIAN. ) SOLID_ANGLE_UNIT ( ) );
#11009=DIRECTION ( 'NONE',  ( -1.000000000000000000, 0.000000000000000000, 0.000000000000000000 ) ) ;
#11065=FACE_OUTER_BOUND ( 'NONE', #1260, .T. ) ;
#11100=DIRECTION ( 'NONE',  ( -1.000000000000000000, 0.000000000000000000, 1.442933311647907116E-16 ) ) ;
#11107=ADVANCED_FACE ( 'NONE', ( #8584 ), #19904, .F. ) ;
#11124=VECTOR ( 'NONE', #17479, 999.9999999999998863 ) ;
#11163=CARTESIAN_POINT ( 'NONE',  ( -10.13407133124522730, 41.92645089659917801, 69.94509975324525897 ) ) ;
#11244=CARTESIAN_POINT ( 'NONE',  ( -8.134906293162361024, 41.92645089659918511, 68.06527860057354928 ) ) ;
#11264=DIRECTION ( 'NONE',  ( -1.000000000000000000, -3.491481338843133355E-15, 1.224646799147353207E-16 ) ) ;
#11293=LINE ( 'NONE', #2809, #20605 ) ;
#11327=CARTESIAN_POINT ( 'NONE',  ( -9.178906393579158163, 42.46645089659918426, 68.06527860057354928 ) ) ;
#11330=ORIENTED_EDGE ( 'NONE', *, *, #21503, .F. ) ;
#11340=FACE_OUTER_BOUND ( 'NONE', #3887, .T. ) ;
#11389=LINE ( 'NONE', #8157, #21186 ) ;
#11420=CARTESIAN_POINT ( 'NONE',  ( -10.05825507651048412, 43.00645089659918341, 69.00503344894275415 ) ) ;
#11426=AXIS2_PLACEMENT_3D ( 'NONE', #11917, #1753, #12027 ) ;
#11459=VERTEX_POINT ( 'NONE', #709 ) ;
#11466=CARTESIAN_POINT ( 'NONE',  ( -8.299557710647832209, 41.92645089659918511, 69.00503344894275415 ) ) ;
#11499=CONICAL_SURFACE ( 'NONE', #8663, 4.575000000000001066, 0.8028514559173934861 ) ;
#11526=CARTESIAN_POINT ( 'NONE',  ( -9.978973617317267397, 43.00645089659918341, 68.06527860057354928 ) ) ;
#11565=EDGE_CURVE ( 'NONE', #18107, #15401, #18581, .T. ) ;
#11590=DIRECTION ( 'NONE',  ( -1.000000000000000000, 0.000000000000000000, 0.000000000000000000 ) ) ;
#11604=ORIENTED_EDGE ( 'NONE', *, *, #11853, .F. ) ;
#11680=CARTESIAN_POINT ( 'NONE',  ( -8.223741455913085474, 41.92645089659918511, 69.94509975324523054 ) ) ;
#11685=DIRECTION ( 'NONE',  ( -1.000000000000000000, 0.000000000000000000, 0.000000000000000000 ) ) ;
#11687=CIRCLE ( 'NONE', #2022, 0.9652499999999990532 ) ;
#11780=CARTESIAN_POINT ( 'NONE',  ( -11.67890639357915816, 42.46645089659918426, 67.85468508031152624 ) ) ;
#11810=ADVANCED_FACE ( 'NONE', ( #21606 ), #14857, .T. ) ;
#11827=DIRECTION ( 'NONE',  ( 1.224646799147353207E-16, 0.000000000000000000, 1.000000000000000000 ) ) ;
#11829=VECTOR ( 'NONE', #13258, 1000.000000000000000 ) ;
#11853=EDGE_CURVE ( 'NONE', #9625, #21235, #19920, .T. ) ;
#11858=CIRCLE ( 'NONE', #14720, 0.9652499999999990532 ) ;
#11885=ORIENTED_EDGE ( 'NONE', *, *, #6818, .F. ) ;
#11891=FACE_OUTER_BOUND ( 'NONE', #14228, .T. ) ;
#11892=ORIENTED_EDGE ( 'NONE', *, *, #4115, .F. ) ;
#11909=DIRECTION ( 'NONE',  ( -1.000000000000000000, 0.000000000000000000, 0.000000000000000000 ) ) ;
#11917=CARTESIAN_POINT ( 'NONE',  ( -12.92890639357915816, 42.46645089659918426, 67.85468508031152624 ) ) ;
#11918=STYLED_ITEM ( 'NONE', ( #15893 ), #7272 ) ;
#11929=DIRECTION ( 'NONE',  ( 1.224646799147353207E-16, 0.000000000000000000, 1.000000000000000000 ) ) ;
#11935=PRODUCT_DEFINITION_FORMATION_WITH_SPECIFIED_SOURCE ( 'ANY', '', #6454, .NOT_KNOWN. ) ;
#11956=DIRECTION ( 'NONE',  ( -1.224646799147353207E-16, -0.000000000000000000, -1.000000000000000000 ) ) ;
#11962=CIRCLE ( 'NONE', #16985, 0.9652499999999990532 ) ;
#11963=ORIENTED_EDGE ( 'NONE', *, *, #19862, .T. ) ;
#12021=CIRCLE ( 'NONE', #2375, 1.162443609680678280 ) ;
#12027=DIRECTION ( 'NONE',  ( 0.000000000000000000, 0.000000000000000000, 1.000000000000000000 ) ) ;
#12029=ORIENTED_EDGE ( 'NONE', *, *, #9427, .F. ) ;
#12030=DIRECTION ( 'NONE',  ( 5.464346504236778158E-17, -0.8949343913984425525, 0.4461977533474361102 ) ) ;
#12043=CONICAL_SURFACE ( 'NONE', #4603, 0.9652499999999990532, 0.06981317007976590994 ) ;
#12056=ORIENTED_EDGE ( 'NONE', *, *, #1043, .F. ) ;
#12058=B_SPLINE_CURVE_WITH_KNOTS ( 'NONE', 3,
 ( #10088, #16898, #11420, #11526 ),
 .UNSPECIFIED., .F., .F.,
 ( 4, 4 ),
 ( 0.001759598105097497350, 0.004588913567995311395 ),
 .UNSPECIFIED. ) ;
#12086=ORIENTED_EDGE ( 'NONE', *, *, #8847, .F. ) ;
#12093=VERTEX_POINT ( 'NONE', #21025 ) ;
#12110=VERTEX_POINT ( 'NONE', #17312 ) ;
#12138=DIRECTION ( 'NONE',  ( -1.000000000000000000, 0.000000000000000000, 0.000000000000000000 ) ) ;
#12143=DIRECTION ( 'NONE',  ( 1.224646799147353207E-16, 0.000000000000000000, 1.000000000000000000 ) ) ;
#12156=FILL_AREA_STYLE ('',( #12255 ) ) ;
#12186=SHAPE_DEFINITION_REPRESENTATION ( #10395, #10840 ) ;
#12196=CARTESIAN_POINT ( 'NONE',  ( -6.728906393579160650, 43.00645089659919762, 70.88527860057354246 ) ) ;
#12200=LINE ( 'NONE', #8978, #10113 ) ;
#12219=FACE_OUTER_BOUND ( 'NONE', #20089, .T. ) ;
#12255=FILL_AREA_STYLE_COLOUR ( '', #8771 ) ;
#12276=UNCERTAINTY_MEASURE_WITH_UNIT (LENGTH_MEASURE( 1.000000000000000082E-05 ), #2697, 'distance_accuracy_value', 'NONE');
#12285=ORIENTED_EDGE ( 'NONE', *, *, #5455, .F. ) ;
#12293=DIRECTION ( 'NONE',  ( -1.224646799147353207E-16, -0.000000000000000000, -1.000000000000000000 ) ) ;
#12342=AXIS2_PLACEMENT_3D ( 'NONE', #6827, #22029, #13510 ) ;
#12343=AXIS2_PLACEMENT_3D ( 'NONE', #13580, #20527, #3067 ) ;
#12441=DIRECTION ( 'NONE',  ( 1.224646799147353207E-16, 0.000000000000000000, 1.000000000000000000 ) ) ;
#12503=EDGE_CURVE ( 'NONE', #21390, #1195, #2662, .T. ) ;
#12507=DIRECTION ( 'NONE',  ( -1.224646799147353207E-16, -0.000000000000000000, -1.000000000000000000 ) ) ;
#12516=ORIENTED_EDGE ( 'NONE', *, *, #4892, .F. ) ;
#12525=ADVANCED_FACE ( 'NONE', ( #13764 ), #18900, .F. ) ;
#12533=FACE_OUTER_BOUND ( 'NONE', #10848, .T. ) ;
#12539=SHAPE_REPRESENTATION_RELATIONSHIP ( 'NONE' , 'NONE' ,  #10840, #7272 ) ;
#12546=EDGE_CURVE ( 'NONE', #16141, #17257, #12835, .T. ) ;
#12580=LINE ( 'NONE', #5691, #1722 ) ;
#12609=DIRECTION ( 'NONE',  ( -1.000000000000000000, 0.000000000000000000, 0.000000000000000000 ) ) ;
#12685=ORIENTED_EDGE ( 'NONE', *, *, #12546, .F. ) ;
#12691=ORIENTED_EDGE ( 'NONE', *, *, #15088, .T. ) ;
#12699=ORIENTED_EDGE ( 'NONE', *, *, #14950, .F. ) ;
#12719=DIRECTION ( 'NONE',  ( 0.4461977533474359991, 1.557891129246304494E-15, -0.8949343913984425525 ) ) ;
#12757=( NAMED_UNIT ( * ) PLANE_ANGLE_UNIT ( ) SI_UNIT ( $, .RADIAN. ) );
#12803=ORIENTED_EDGE ( 'NONE', *, *, #5455, .T. ) ;
#12823=EDGE_CURVE ( 'NONE', #1195, #20955, #15417, .T. ) ;
#12835=LINE ( 'NONE', #9488, #2077 ) ;
#12852=FACE_OUTER_BOUND ( 'NONE', #15542, .T. ) ;
#12864=DIRECTION ( 'NONE',  ( 1.000000000000000000, -1.038507728162729222E-16, -1.357958710150075923E-16 ) ) ;
#12872=CARTESIAN_POINT ( 'NONE',  ( -8.638906393579159015, 43.51045099701597962, 68.06527860057354928 ) ) ;
#12891=ORIENTED_EDGE ( 'NONE', *, *, #10323, .T. ) ;
#12896=ORIENTED_EDGE ( 'NONE', *, *, #6065, .T. ) ;
#12925=ORIENTED_EDGE ( 'NONE', *, *, #983, .T. ) ;
#12999=VERTEX_POINT ( 'NONE', #6130 ) ;
#13006=ADVANCED_FACE ( 'NONE', ( #16601 ), #1394, .F. ) ;
#13014=ORIENTED_EDGE ( 'NONE', *, *, #14136, .T. ) ;
#13017=EDGE_CURVE ( 'NONE', #6925, #10275, #7807, .T. ) ;
#13063=DIRECTION ( 'NONE',  ( 0.8949343913984425525, 3.124646727056599230E-15, 0.4461977533474359991 ) ) ;
#13074=DIRECTION ( 'NONE',  ( 1.095978537872987245E-16, -0.4461977533474357216, 0.8949343913984425525 ) ) ;
#13088=AXIS2_PLACEMENT_3D ( 'NONE', #1619, #1285, #10138 ) ;
#13095=ORIENTED_EDGE ( 'NONE', *, *, #8847, .T. ) ;
#13100=EDGE_CURVE ( 'NONE', #21631, #2238, #18299, .T. ) ;
#13106=VECTOR ( 'NONE', #13653, 1000.000000000000000 ) ;
#13126=ORIENTED_EDGE ( 'NONE', *, *, #5313, .F. ) ;
#13149=ORIENTED_EDGE ( 'NONE', *, *, #4785, .T. ) ;
#13172=AXIS2_PLACEMENT_3D ( 'NONE', #21605, #13063, #12719 ) ;
#13187=CARTESIAN_POINT ( 'NONE',  ( -9.718906393579157310, 41.43704565779017202, 70.88527860057354246 ) ) ;
#13194=ADVANCED_FACE ( 'NONE', ( #22124 ), #8781, .T. ) ;
#13204=LINE ( 'NONE', #16547, #4885 ) ;
#13232=ORIENTED_EDGE ( 'NONE', *, *, #14927, .F. ) ;
#13240=ORIENTED_EDGE ( 'NONE', *, *, #1858, .T. ) ;
#13258=DIRECTION ( 'NONE',  ( 1.224646799147353207E-16, 0.000000000000000000, 1.000000000000000000 ) ) ;
#13320=ORIENTED_EDGE ( 'NONE', *, *, #12503, .F. ) ;
#13365=DIRECTION ( 'NONE',  ( 1.000000000000000000, 3.358721889151030981E-15, -1.224646799147353207E-16 ) ) ;
#13399=CARTESIAN_POINT ( 'NONE',  ( -10.22290649399595353, 43.00645089659918341, 68.06527860057354928 ) ) ;
#13411=CARTESIAN_POINT ( 'NONE',  ( -9.718906393579157310, 43.42161583426526761, 69.94509975324525897 ) ) ;
#13454=DIRECTION ( 'NONE',  ( -3.387630566026860322E-15, 1.000000000000000000, -1.333119110027185404E-17 ) ) ;
#13461=VECTOR ( 'NONE', #18708, 1000.000000000000114 ) ;
#13493=AXIS2_PLACEMENT_3D ( 'NONE', #21138, #16279, #16172 ) ;
#13510=DIRECTION ( 'NONE',  ( -1.000000000000000000, 0.000000000000000000, 0.000000000000000000 ) ) ;
#13514=ORIENTED_EDGE ( 'NONE', *, *, #9427, .T. ) ;
#13515=DIRECTION ( 'NONE',  ( -1.224646799147353207E-16, -0.000000000000000000, -1.000000000000000000 ) ) ;
#13518=ORIENTED_EDGE ( 'NONE', *, *, #9319, .T. ) ;
#13526=VERTEX_POINT ( 'NONE', #8322 ) ;
#13580=CARTESIAN_POINT ( 'NONE',  ( -9.178906393579158163, 42.46645089659918426, 67.85468508031152624 ) ) ;
#13596=ORIENTED_EDGE ( 'NONE', *, *, #4743, .F. ) ;
#13653=DIRECTION ( 'NONE',  ( -1.000000000000000000, -3.543406725251269872E-15, 1.224646799147353207E-16 ) ) ;
#13685=CARTESIAN_POINT ( 'NONE',  ( -11.62890639357915923, 43.00645089659917630, 70.88527860057354246 ) ) ;
#13710=FACE_OUTER_BOUND ( 'NONE', #13901, .T. ) ;
#13715=ORIENTED_EDGE ( 'NONE', *, *, #6818, .T. ) ;
#13727=ORIENTED_EDGE ( 'NONE', *, *, #13017, .T. ) ;
#13760=ORIENTED_EDGE ( 'NONE', *, *, #12823, .T. ) ;
#13764=FACE_OUTER_BOUND ( 'NONE', #1721, .T. ) ;
#13824=DIRECTION ( 'NONE',  ( -1.000000000000000000, 0.000000000000000000, 0.000000000000000000 ) ) ;
#13834=FACE_OUTER_BOUND ( 'NONE', #15566, .T. ) ;
#13901=EDGE_LOOP ( 'NONE', ( #2371, #7182, #21594, #13922 ) ) ;
#13922=ORIENTED_EDGE ( 'NONE', *, *, #9504, .F. ) ;
#13930=FACE_OUTER_BOUND ( 'NONE', #1776, .T. ) ;
#13968=AXIS2_PLACEMENT_3D ( 'NONE', #14145, #16043, #2407 ) ;
#13987=EDGE_CURVE ( 'NONE', #13526, #15347, #11858, .T. ) ;
#14003=ORIENTED_EDGE ( 'NONE', *, *, #4452, .T. ) ;
#14005=CARTESIAN_POINT ( 'NONE',  ( -5.428906393579158163, 42.46645089659918426, 67.85468508031152624 ) ) ;
#14011=AXIS2_PLACEMENT_3D ( 'NONE', #19030, #19131, #3696 ) ;
#14098=CARTESIAN_POINT ( 'NONE',  ( -9.178906393579158163, 42.46645089659918426, 70.88527860057354246 ) ) ;
#14105=SURFACE_SIDE_STYLE ('',( #7313 ) ) ;
#14119=EDGE_CURVE ( 'NONE', #299, #6925, #5472, .T. ) ;
#14136=EDGE_CURVE ( 'NONE', #183, #12999, #531, .T. ) ;
#14145=CARTESIAN_POINT ( 'NONE',  ( -10.22290649399595353, 43.00645089659918341, 68.06527860057354928 ) ) ;
#14197=AXIS2_PLACEMENT_3D ( 'NONE', #17724, #17519, #9237 ) ;
#14224=DIRECTION ( 'NONE',  ( -1.000000000000000000, 0.000000000000000000, 0.000000000000000000 ) ) ;
#14228=EDGE_LOOP ( 'NONE', ( #1203, #15322, #17292, #9632 ) ) ;
#14230=( NAMED_UNIT ( * ) SI_UNIT ( $, .STERADIAN. ) SOLID_ANGLE_UNIT ( ) );
#14260=ORIENTED_EDGE ( 'NONE', *, *, #19862, .F. ) ;
#14269=CARTESIAN_POINT ( 'NONE',  ( -9.178906393579161715, 42.46645089659918426, 61.53912392244307483 ) ) ;
#14279=VERTEX_POINT ( 'NONE', #13187 ) ;
#14318=ORIENTED_EDGE ( 'NONE', *, *, #19445, .F. ) ;
#14321=ORIENTED_EDGE ( 'NONE', *, *, #21733, .T. ) ;
#14332=PLANE ( 'NONE',  #21986 ) ;
#14392=ORIENTED_EDGE ( 'NONE', *, *, #19445, .T. ) ;
#14407=CARTESIAN_POINT ( 'NONE',  ( -9.718906393579157310, 43.49585613540820361, 70.88527860057354246 ) ) ;
#14415=ORIENTED_EDGE ( 'NONE', *, *, #13017, .F. ) ;
#14420=DIRECTION ( 'NONE',  ( 1.224646799147353207E-16, 0.000000000000000000, 1.000000000000000000 ) ) ;
#14443=CARTESIAN_POINT ( 'NONE',  ( -9.178906393579158163, 42.46645089659918426, 68.06527860057354928 ) ) ;
#14452=VERTEX_POINT ( 'NONE', #377 ) ;
#14479=CARTESIAN_POINT ( 'NONE',  ( -8.638906393579159015, 40.01645089659919563, 70.88527860057354246 ) ) ;
#14498=EDGE_LOOP ( 'NONE', ( #11892, #1924, #12803, #12896 ) ) ;
#14529=PLANE ( 'NONE',  #6530 ) ;
#14531=DIRECTION ( 'NONE',  ( -0.9510565162951554186, 0.000000000000000000, 0.3090169943749416781 ) ) ;
#14579=DIRECTION ( 'NONE',  ( -1.000000000000000000, 0.000000000000000000, 0.000000000000000000 ) ) ;
#14593=VECTOR ( 'NONE', #15182, 1000.000000000000000 ) ;
#14597=LINE ( 'NONE', #21451, #6297 ) ;
#14632=AXIS2_PLACEMENT_3D ( 'NONE', #17618, #9020, #20776 ) ;
#14645=VECTOR ( 'NONE', #10386, 1000.000000000000000 ) ;
#14662=EDGE_CURVE ( 'NONE', #3680, #12999, #52, .T. ) ;
#14671=VERTEX_POINT ( 'NONE', #6211 ) ;
#14720=AXIS2_PLACEMENT_3D ( 'NONE', #21846, #6521, #5160 ) ;
#14727=ORIENTED_EDGE ( 'NONE', *, *, #13100, .F. ) ;
#14755=CARTESIAN_POINT ( 'NONE',  ( -10.22290649399595353, 43.00645089659918341, 68.06527860057354928 ) ) ;
#14778=DIRECTION ( 'NONE',  ( -3.290703158753225287E-15, 1.000000000000000000, 4.029949090311222146E-31 ) ) ;
#14798=CARTESIAN_POINT ( 'NONE',  ( -9.178906393579158163, 42.46645089659918426, 68.06527860057354928 ) ) ;
#14817=VERTEX_POINT ( 'NONE', #20745 ) ;
#14821=DIRECTION ( 'NONE',  ( -3.387630566026860322E-15, 1.000000000000000000, -1.333119110027185404E-17 ) ) ;
#14822=ADVANCED_FACE ( 'NONE', ( #3621 ), #3178, .T. ) ;
#14857=PLANE ( 'NONE',  #6369 ) ;
#14878=CARTESIAN_POINT ( 'NONE',  ( -13.75390639357915923, 42.46645089659918426, 74.06027860057353962 ) ) ;
#14927=EDGE_CURVE ( 'NONE', #14671, #15347, #355, .T. ) ;
#14950=EDGE_CURVE ( 'NONE', #2238, #12093, #17360, .T. ) ;
#14980=EDGE_CURVE ( 'NONE', #2238, #12110, #5044, .T. ) ;
#14986=ADVANCED_FACE ( 'NONE', ( #10512 ), #20816, .F. ) ;
#14992=CIRCLE ( 'NONE', #7854, 0.9652499999999990532 ) ;
#15003=CIRCLE ( 'NONE', #16442, 2.500000000000000444 ) ;
#15021=VECTOR ( 'NONE', #14531, 1000.000000000000114 ) ;
#15043=DIRECTION ( 'NONE',  ( 2.688368618483499901E-15, -1.000000000000000000, -3.292302023554010137E-31 ) ) ;
#15061=ORIENTED_EDGE ( 'NONE', *, *, #5955, .F. ) ;
#15088=EDGE_CURVE ( 'NONE', #17645, #14671, #15966, .T. ) ;
#15161=VERTEX_POINT ( 'NONE', #17440 ) ;
#15173=DIRECTION ( 'NONE',  ( -1.000000000000000000, 0.000000000000000000, 1.224646799147353207E-16 ) ) ;
#15177=DIRECTION ( 'NONE',  ( 1.000000000000000000, -1.038507728162729222E-16, -1.357958710150075923E-16 ) ) ;
#15182=DIRECTION ( 'NONE',  ( 1.000000000000000000, -2.007781800899081911E-16, -1.224646799147353207E-16 ) ) ;
#15203=AXIS2_PLACEMENT_3D ( 'NONE', #5878, #4405, #11009 ) ;
#15235=AXIS2_PLACEMENT_3D ( 'NONE', #9723, #1420, #11590 ) ;
#15244=ORIENTED_EDGE ( 'NONE', *, *, #6996, .F. ) ;
#15287=EDGE_CURVE ( 'NONE', #22112, #17384, #11389, .T. ) ;
#15292=VECTOR ( 'NONE', #15043, 1000.000000000000000 ) ;
#15310=CARTESIAN_POINT ( 'NONE',  ( -9.178906393579158163, 42.46645089659918426, 68.06527860057354928 ) ) ;
#15320=DIRECTION ( 'NONE',  ( 1.000000000000000000, 0.000000000000000000, -1.224646799147353207E-16 ) ) ;
#15322=ORIENTED_EDGE ( 'NONE', *, *, #1043, .T. ) ;
#15346=ORIENTED_EDGE ( 'NONE', *, *, #8333, .T. ) ;
#15347=VERTEX_POINT ( 'NONE', #2899 ) ;
#15401=VERTEX_POINT ( 'NONE', #10387 ) ;
#15405=CARTESIAN_POINT ( 'NONE',  ( -9.718906393579157310, 43.51045099701597252, 68.06527860057354928 ) ) ;
#15412=ORIENTED_EDGE ( 'NONE', *, *, #17963, .F. ) ;
#15417=LINE ( 'NONE', #8371, #14593 ) ;
#15420=ADVANCED_FACE ( 'NONE', ( #10274 ), #6825, .T. ) ;
#15426=ORIENTED_EDGE ( 'NONE', *, *, #11565, .F. ) ;
#15442=EDGE_CURVE ( 'NONE', #9924, #14817, #8785, .T. ) ;
#15507=CYLINDRICAL_SURFACE ( 'NONE', #12342, 4.575000000000001066 ) ;
#15514=CARTESIAN_POINT ( 'NONE',  ( -8.299557710647819775, 43.00645089659919051, 69.00503344894293889 ) ) ;
#15527=CARTESIAN_POINT ( 'NONE',  ( -8.638906393579159015, 43.51045099701597252, 68.06527860057354928 ) ) ;
#15542=EDGE_LOOP ( 'NONE', ( #12056, #37, #3202, #14318 ) ) ;
#15566=EDGE_LOOP ( 'NONE', ( #18535, #4362 ) ) ;
#15584=CARTESIAN_POINT ( 'NONE',  ( -9.178906393579158163, 42.46645089659918426, 74.06027860057353962 ) ) ;
#15733=DIRECTION ( 'NONE',  ( -1.224646799147353207E-16, -0.000000000000000000, -1.000000000000000000 ) ) ;
#15770=AXIS2_PLACEMENT_3D ( 'NONE', #15527, #3353, #201 ) ;
#15823=DIRECTION ( 'NONE',  ( -1.000000000000000000, 0.000000000000000000, 0.000000000000000000 ) ) ;
#15883=CARTESIAN_POINT ( 'NONE',  ( -8.638906393579159015, 41.66638367286108746, 68.06527860057354928 ) ) ;
#15893=PRESENTATION_STYLE_ASSIGNMENT (( #16120 ) ) ;
#15894=FACE_OUTER_BOUND ( 'NONE', #21892, .T. ) ;
#15897=AXIS2_PLACEMENT_3D ( 'NONE', #16369, #21543, #9677 ) ;
#15961=ORIENTED_EDGE ( 'NONE', *, *, #172, .F. ) ;
#15966=LINE ( 'NONE', #7382, #4025 ) ;
#16028=ORIENTED_EDGE ( 'NONE', *, *, #19525, .F. ) ;
#16035=VERTEX_POINT ( 'NONE', #9001 ) ;
#16043=DIRECTION ( 'NONE',  ( 3.543406725251269872E-15, -1.000000000000000000, -5.100473277356134011E-17 ) ) ;
#16063=ADVANCED_FACE ( 'NONE', ( #807 ), #20597, .F. ) ;
#16072=B_SPLINE_CURVE_WITH_KNOTS ( 'NONE', 3,
 ( #10698, #19606, #10477, #4279 ),
 .UNSPECIFIED., .F., .F.,
 ( 4, 4 ),
 ( 0.001759598111914162421, 0.004588913574811922039 ),
 .UNSPECIFIED. ) ;
#16087=PLANE ( 'NONE',  #13172 ) ;
#16099=CARTESIAN_POINT ( 'NONE',  ( -8.638906393579159015, 41.42245079618239600, 68.06527860057354928 ) ) ;
#16120=SURFACE_STYLE_USAGE ( .BOTH. , #14105 ) ;
#16141=VERTEX_POINT ( 'NONE', #9433 ) ;
#16146=AXIS2_PLACEMENT_3D ( 'NONE', #5359, #15177, #18998 ) ;
#16149=ORIENTED_EDGE ( 'NONE', *, *, #19060, .F. ) ;
#16172=DIRECTION ( 'NONE',  ( -1.000000000000000000, 0.000000000000000000, 0.000000000000000000 ) ) ;
#16186=CARTESIAN_POINT ( 'NONE',  ( -10.05825507651049655, 41.92645089659917801, 69.00503344894293889 ) ) ;
#16195=VECTOR ( 'NONE', #9252, 1000.000000000000114 ) ;
#16226=DIRECTION ( 'NONE',  ( 1.000000000000000000, 0.000000000000000000, 0.000000000000000000 ) ) ;
#16233=CARTESIAN_POINT ( 'NONE',  ( -8.638906393579159015, 40.01645089659919563, 70.88527860057354246 ) ) ;
#16248=ADVANCED_FACE ( 'NONE', ( #16340 ), #21190, .F. ) ;
#16258=CARTESIAN_POINT ( 'NONE',  ( -8.638906393579159015, 43.51045099701597252, 68.06527860057354928 ) ) ;
#16279=DIRECTION ( 'NONE',  ( -1.224646799147353207E-16, -0.000000000000000000, -1.000000000000000000 ) ) ;
#16297=DIRECTION ( 'NONE',  ( -1.038507728162729346E-16, -1.000000000000000000, 1.271805165184275985E-32 ) ) ;
#16304=EDGE_CURVE ( 'NONE', #7942, #3680, #18253, .T. ) ;
#16340=FACE_OUTER_BOUND ( 'NONE', #17202, .T. ) ;
#16344=ORIENTED_EDGE ( 'NONE', *, *, #6834, .F. ) ;
#16368=AXIS2_PLACEMENT_3D ( 'NONE', #19067, #12441, #17492 ) ;
#16369=CARTESIAN_POINT ( 'NONE',  ( -9.178906393579158163, 42.46645089659918426, 70.88527860057354246 ) ) ;
#16400=DIRECTION ( 'NONE',  ( -1.224646799147353207E-16, 0.000000000000000000, -1.000000000000000000 ) ) ;
#16442=AXIS2_PLACEMENT_3D ( 'NONE', #19315, #9024, #15823 ) ;
#16458=LINE ( 'NONE', #9530, #6004 ) ;
#16475=ORIENTED_EDGE ( 'NONE', *, *, #15287, .T. ) ;
#16537=DIRECTION ( 'NONE',  ( -1.000000000000000000, 8.031127203596333560E-16, 1.224646799147353207E-16 ) ) ;
#16547=CARTESIAN_POINT ( 'NONE',  ( -9.718906393579157310, 44.91645089659918710, 70.88527860057354246 ) ) ;
#16601=FACE_OUTER_BOUND ( 'NONE', #286, .T. ) ;
#16632=ORIENTED_EDGE ( 'NONE', *, *, #19060, .T. ) ;
#16638=CARTESIAN_POINT ( 'NONE',  ( -8.638906393579159015, 41.42245079618239600, 68.06527860057354928 ) ) ;
#16652=CARTESIAN_POINT ( 'NONE',  ( -9.718906393579157310, 43.34579957953053508, 69.00503344894293889 ) ) ;
#16655=AXIS2_PLACEMENT_3D ( 'NONE', #9419, #2595, #1127 ) ;
#16732=ORIENTED_EDGE ( 'NONE', *, *, #3030, .F. ) ;
#16760=DIRECTION ( 'NONE',  ( -1.000000000000000000, 0.000000000000000000, 0.000000000000000000 ) ) ;
#16769=LINE ( 'NONE', #6841, #10271 ) ;
#16775=CIRCLE ( 'NONE', #19640, 0.9652499999999990532 ) ;
#16785=LINE ( 'NONE', #14878, #1597 ) ;
#16804=DIRECTION ( 'NONE',  ( -0.7193398003386523021, 0.000000000000000000, 0.6946583704589960329 ) ) ;
#16890=CONICAL_SURFACE ( 'NONE', #19043, 0.9652499999999990532, 0.06981317007976590994 ) ;
#16898=CARTESIAN_POINT ( 'NONE',  ( -10.13407133124522908, 43.00645089659918341, 69.94509975324523054 ) ) ;
#16925=ORIENTED_EDGE ( 'NONE', *, *, #13100, .T. ) ;
#16940=CARTESIAN_POINT ( 'NONE',  ( -8.149501154770138811, 41.92645089659918511, 70.88527860057354246 ) ) ;
#16948=DIRECTION ( 'NONE',  ( -1.224646799147353207E-16, -0.000000000000000000, -1.000000000000000000 ) ) ;
#16985=AXIS2_PLACEMENT_3D ( 'NONE', #3570, #13515, #20358 ) ;
#16987=ORIENTED_EDGE ( 'NONE', *, *, #3325, .F. ) ;
#16994=DIRECTION ( 'NONE',  ( -2.128201741475310638E-16, -0.4461977533474360547, -0.8949343913984424415 ) ) ;
#17033=DIRECTION ( 'NONE',  ( -1.000000000000000000, 0.000000000000000000, 0.000000000000000000 ) ) ;
#17084=FACE_OUTER_BOUND ( 'NONE', #2884, .T. ) ;
#17103=DIRECTION ( 'NONE',  ( 3.491481338843133355E-15, -1.000000000000000000, -4.275831445896958607E-31 ) ) ;
#17146=CIRCLE ( 'NONE', #14632, 1.162443609680678280 ) ;
#17182=VERTEX_POINT ( 'NONE', #10226 ) ;
#17188=CARTESIAN_POINT ( 'NONE',  ( -9.718906393579157310, 44.91645089659918710, 70.88527860057354246 ) ) ;
#17202=EDGE_LOOP ( 'NONE', ( #1849, #21107, #12925, #5461 ) ) ;
#17203=( NAMED_UNIT ( * ) PLANE_ANGLE_UNIT ( ) SI_UNIT ( $, .RADIAN. ) );
#17239=ORIENTED_EDGE ( 'NONE', *, *, #10827, .F. ) ;
#17245=LINE ( 'NONE', #12196, #9879 ) ;
#17257=VERTEX_POINT ( 'NONE', #8881 ) ;
#17279=EDGE_CURVE ( 'NONE', #14452, #14817, #21382, .T. ) ;
#17292=ORIENTED_EDGE ( 'NONE', *, *, #9504, .T. ) ;
#17303=DIRECTION ( 'NONE',  ( 1.000000000000000000, 0.000000000000000000, -1.224646799147353207E-16 ) ) ;
#17312=CARTESIAN_POINT ( 'NONE',  ( -6.728906393579160650, 43.00645089659919762, 70.88527860057354246 ) ) ;
#17333=EDGE_LOOP ( 'NONE', ( #1562, #20820, #17239, #21060 ) ) ;
#17360=LINE ( 'NONE', #2032, #11124 ) ;
#17384=VERTEX_POINT ( 'NONE', #4060 ) ;
#17391=EDGE_LOOP ( 'NONE', ( #13240, #1783, #13320, #18618 ) ) ;
#17440=CARTESIAN_POINT ( 'NONE',  ( -10.20831163238817219, 41.92645089659918511, 70.88527860057354246 ) ) ;
#17451=DIRECTION ( 'NONE',  ( 0.9510565162951554186, -1.164708318489094811E-16, 0.3090169943749414561 ) ) ;
#17479=DIRECTION ( 'NONE',  ( -0.4461977533474359436, -1.523483689126226091E-15, -0.8949343913984425525 ) ) ;
#17490=ADVANCED_FACE ( 'NONE', ( #18141 ), #9763, .T. ) ;
#17492=DIRECTION ( 'NONE',  ( -1.000000000000000000, 0.000000000000000000, 1.224646799147353207E-16 ) ) ;
#17493=AXIS2_PLACEMENT_3D ( 'NONE', #9767, #1237, #16226 ) ;
#17519=DIRECTION ( 'NONE',  ( 1.224646799147353207E-16, 0.000000000000000000, 1.000000000000000000 ) ) ;
#17522=FACE_OUTER_BOUND ( 'NONE', #9044, .T. ) ;
#17574=ORIENTED_EDGE ( 'NONE', *, *, #7050, .F. ) ;
#17600=FACE_BOUND ( 'NONE', #10262, .T. ) ;
#17618=CARTESIAN_POINT ( 'NONE',  ( -9.178906393579158163, 42.46645089659918426, 70.88527860057354246 ) ) ;
#17635=( LENGTH_UNIT ( ) NAMED_UNIT ( * ) SI_UNIT ( .MILLI., .METRE. ) );
#17645=VERTEX_POINT ( 'NONE', #8202 ) ;
#17724=CARTESIAN_POINT ( 'NONE',  ( -9.178906393579158163, 42.46645089659918426, 74.06027860057353962 ) ) ;
#17796=DIRECTION ( 'NONE',  ( -5.192538640813645496E-17, 1.000000000000000000, 6.359025825921378559E-33 ) ) ;
#17806=AXIS2_PLACEMENT_3D ( 'NONE', #5924, #5827, #12609 ) ;
#17846=CARTESIAN_POINT ( 'NONE',  ( -9.718906393579157310, 41.42245079618239600, 68.06527860057354928 ) ) ;
#17894=FACE_OUTER_BOUND ( 'NONE', #17391, .T. ) ;
#17902=VECTOR ( 'NONE', #2965, 1000.000000000000000 ) ;
#17914=ORIENTED_EDGE ( 'NONE', *, *, #16304, .T. ) ;
#17963=EDGE_CURVE ( 'NONE', #21390, #18170, #16769, .T. ) ;
#18008=ORIENTED_EDGE ( 'NONE', *, *, #1858, .F. ) ;
#18021=DIRECTION ( 'NONE',  ( 5.192538640813645496E-17, -1.000000000000000000, -6.359025825921378559E-33 ) ) ;
#18030=DIRECTION ( 'NONE',  ( -1.000000000000000000, 0.000000000000000000, 0.000000000000000000 ) ) ;
#18046=CARTESIAN_POINT ( 'NONE',  ( -8.134906293162368129, 43.00645089659919051, 68.06527860057354928 ) ) ;
#18101=EDGE_CURVE ( 'NONE', #18107, #17257, #11687, .T. ) ;
#18107=VERTEX_POINT ( 'NONE', #6178 ) ;
#18122=CARTESIAN_POINT ( 'NONE',  ( -8.134906293162368129, 43.00645089659919051, 68.06527860057354928 ) ) ;
#18141=FACE_OUTER_BOUND ( 'NONE', #17333, .T. ) ;
#18146=ADVANCED_FACE ( 'NONE', ( #8183 ), #952, .T. ) ;
#18153=ORIENTED_EDGE ( 'NONE', *, *, #6065, .F. ) ;
#18157=CIRCLE ( 'NONE', #8128, 0.9652499999999990532 ) ;
#18170=VERTEX_POINT ( 'NONE', #7962 ) ;
#18221=CARTESIAN_POINT ( 'NONE',  ( -8.378839169841052481, 41.92645089659918511, 68.06527860057354928 ) ) ;
#18223=ORIENTED_EDGE ( 'NONE', *, *, #21733, .F. ) ;
#18253=LINE ( 'NONE', #686, #9888 ) ;
#18261=EDGE_CURVE ( 'NONE', #13526, #1195, #3352, .T. ) ;
#18299=LINE ( 'NONE', #2975, #6188 ) ;
#18304=VECTOR ( 'NONE', #17451, 1000.000000000000114 ) ;
#18341=CARTESIAN_POINT ( 'NONE',  ( -9.718906393579157310, 43.26651812033729527, 68.06527860057354928 ) ) ;
#18359=ORIENTED_EDGE ( 'NONE', *, *, #4624, .F. ) ;
#18380=ORIENTED_EDGE ( 'NONE', *, *, #6517, .T. ) ;
#18396=LINE ( 'NONE', #5099, #20341 ) ;
#18404=CARTESIAN_POINT ( 'NONE',  ( -8.638906393579159015, 43.51045099701597962, 68.06527860057354928 ) ) ;
#18494=ORIENTED_EDGE ( 'NONE', *, *, #1809, .T. ) ;
#18535=ORIENTED_EDGE ( 'NONE', *, *, #7835, .T. ) ;
#18581=LINE ( 'NONE', #1898, #13106 ) ;
#18593=ORIENTED_EDGE ( 'NONE', *, *, #4892, .T. ) ;
#18600=ADVANCED_FACE ( 'NONE', ( #13710 ), #616, .F. ) ;
#18618=ORIENTED_EDGE ( 'NONE', *, *, #17963, .T. ) ;
#18626=DIRECTION ( 'NONE',  ( 1.224646799147353207E-16, 0.000000000000000000, 1.000000000000000000 ) ) ;
#18666=ORIENTED_EDGE ( 'NONE', *, *, #14950, .T. ) ;
#18704=PRODUCT_DEFINITION_CONTEXT ( 'detailed design', #9155, 'design' ) ;
#18708=DIRECTION ( 'NONE',  ( 0.4461977533474357216, 1.626706009486458344E-15, -0.8949343913984425525 ) ) ;
#18737=CARTESIAN_POINT ( 'NONE',  ( -8.378839169841052481, 41.92645089659918511, 68.06527860057354928 ) ) ;
#18747=PLANE ( 'NONE',  #8068 ) ;
#18797=AXIS2_PLACEMENT_3D ( 'NONE', #10970, #12293, #19047 ) ;
#18866=AXIS2_PLACEMENT_3D ( 'NONE', #718, #2403, #12138 ) ;
#18879=DIRECTION ( 'NONE',  ( -1.095978537872987122E-16, -0.4461977533474360547, -0.8949343913984424415 ) ) ;
#18900=CONICAL_SURFACE ( 'NONE', #17806, 0.9652499999999990532, 0.06981317007976590994 ) ;
#18938=ORIENTED_EDGE ( 'NONE', *, *, #18261, .T. ) ;
#18998=DIRECTION ( 'NONE',  ( 1.038507728162729222E-16, 1.000000000000000000, -1.271805165184275985E-32 ) ) ;
#19030=CARTESIAN_POINT ( 'NONE',  ( -9.178906393579158163, 42.46645089659918426, 70.38908280829822672 ) ) ;
#19043=AXIS2_PLACEMENT_3D ( 'NONE', #11327, #20077, #9549 ) ;
#19047=DIRECTION ( 'NONE',  ( -1.000000000000000000, 0.000000000000000000, 0.000000000000000000 ) ) ;
#19052=DIRECTION ( 'NONE',  ( 1.000000000000000000, 3.358721889151030981E-15, -1.224646799147353207E-16 ) ) ;
#19056=CARTESIAN_POINT ( 'NONE',  ( -10.22290649399594642, 41.92645089659918511, 68.06527860057354928 ) ) ;
#19060=EDGE_CURVE ( 'NONE', #17384, #17645, #1388, .T. ) ;
#19067=CARTESIAN_POINT ( 'NONE',  ( -9.178906393579158163, 42.46645089659918426, 70.88527860057354246 ) ) ;
#19091=CARTESIAN_POINT ( 'NONE',  ( -13.75390639357915923, 42.46645089659918426, 70.88527860057354246 ) ) ;
#19130=ADVANCED_FACE ( 'NONE', ( #12219, #17600 ), #5656, .T. ) ;
#19131=DIRECTION ( 'NONE',  ( -1.224646799147353207E-16, -0.000000000000000000, -1.000000000000000000 ) ) ;
#19198=EDGE_LOOP ( 'NONE', ( #13514, #8001, #16344, #13095 ) ) ;
#19238=ORIENTED_EDGE ( 'NONE', *, *, #4624, .T. ) ;
#19279=AXIS2_PLACEMENT_3D ( 'NONE', #19452, #12507, #10626 ) ;
#19303=EDGE_CURVE ( 'NONE', #17257, #11459, #18157, .T. ) ;
#19315=CARTESIAN_POINT ( 'NONE',  ( -9.178906393579158163, 42.46645089659918426, 67.85468508031152624 ) ) ;
#19320=CARTESIAN_POINT ( 'NONE',  ( -9.178906393579158163, 42.46645089659918426, 68.75385983073485363 ) ) ;
#19367=ORIENTED_EDGE ( 'NONE', *, *, #19386, .F. ) ;
#19384=DIRECTION ( 'NONE',  ( 1.038507728162729222E-16, 1.000000000000000000, -1.271805165184275985E-32 ) ) ;
#19386=EDGE_CURVE ( 'NONE', #17384, #15401, #5069, .T. ) ;
#19427=DIRECTION ( 'NONE',  ( -1.000000000000000000, 0.000000000000000000, 0.000000000000000000 ) ) ;
#19430=CARTESIAN_POINT ( 'NONE',  ( -8.378839169841056034, 43.00645089659919051, 68.06527860057354928 ) ) ;
#19445=EDGE_CURVE ( 'NONE', #17182, #299, #4838, .T. ) ;
#19452=CARTESIAN_POINT ( 'NONE',  ( -9.178906393579158163, 42.46645089659918426, 68.06527860057354928 ) ) ;
#19460=AXIS2_PLACEMENT_3D ( 'NONE', #14098, #20949, #14224 ) ;
#19473=( GEOMETRIC_REPRESENTATION_CONTEXT ( 3 ) GLOBAL_UNCERTAINTY_ASSIGNED_CONTEXT ( ( #21634 ) ) GLOBAL_UNIT_ASSIGNED_CONTEXT ( ( #17635, #17203, #4009 ) ) REPRESENTATION_CONTEXT ( 'NONE', 'WORKASPACE' ) );
#19525=EDGE_CURVE ( 'NONE', #12110, #538, #17245, .T. ) ;
#19531=DIRECTION ( 'NONE',  ( -1.224646799147353207E-16, -0.000000000000000000, -1.000000000000000000 ) ) ;
#19606=CARTESIAN_POINT ( 'NONE',  ( -8.638906393579159015, 43.42161583426526761, 69.94509975324525897 ) ) ;
#19613=EDGE_CURVE ( 'NONE', #20955, #20601, #11293, .T. ) ;
#19640=AXIS2_PLACEMENT_3D ( 'NONE', #10217, #20517, #17033 ) ;
#19723=DIRECTION ( 'NONE',  ( -1.000000000000000000, -5.192538640813645496E-17, 7.145994714117440585E-17 ) ) ;
#19742=ADVANCED_FACE ( 'NONE', ( #22154 ), #15507, .T. ) ;
#19748=DIRECTION ( 'NONE',  ( -0.8949343913984425525, -2.944963428651749748E-15, 0.4461977533474358326 ) ) ;
#19772=ORIENTED_EDGE ( 'NONE', *, *, #19613, .F. ) ;
#19862=EDGE_CURVE ( 'NONE', #22112, #3651, #12021, .T. ) ;
#19866=CIRCLE ( 'NONE', #15203, 4.575000000000001066 ) ;
#19879=PLANE ( 'NONE',  #21842 ) ;
#19880=APPLICATION_CONTEXT ( 'automotive_design' ) ;
#19904=CONICAL_SURFACE ( 'NONE', #13088, 3077.683537175317724, 1.256637061435923464 ) ;
#19906=CIRCLE ( 'NONE', #15235, 0.9652499999999990532 ) ;
#19920=LINE ( 'NONE', #20035, #2415 ) ;
#19933=DIRECTION ( 'NONE',  ( -1.000000000000000000, 0.000000000000000000, 0.000000000000000000 ) ) ;
#19941=CARTESIAN_POINT ( 'NONE',  ( -9.718906393579157310, 41.51128595893310802, 69.94509975324525897 ) ) ;
#20007=ORIENTED_EDGE ( 'NONE', *, *, #13987, .T. ) ;
#20035=CARTESIAN_POINT ( 'NONE',  ( -8.638906393579159015, 44.91645089659918710, 70.88527860057354246 ) ) ;
#20044=DIRECTION ( 'NONE',  ( -1.000000000000000000, 0.000000000000000000, 0.000000000000000000 ) ) ;
#20077=DIRECTION ( 'NONE',  ( 1.224646799147353207E-16, 0.000000000000000000, 1.000000000000000000 ) ) ;
#20089=EDGE_LOOP ( 'NONE', ( #8666, #6837 ) ) ;
#20139=ORIENTED_EDGE ( 'NONE', *, *, #15442, .F. ) ;
#20177=DIRECTION ( 'NONE',  ( -1.224646799147353207E-16, -0.000000000000000000, -1.000000000000000000 ) ) ;
#20201=CARTESIAN_POINT ( 'NONE',  ( -8.638906393579159015, 43.51045099701597252, 68.06527860057354928 ) ) ;
#20220=CIRCLE ( 'NONE', #18797, 2.500000000000000444 ) ;
#20250=CARTESIAN_POINT ( 'NONE',  ( -13.75390639357915923, 42.46645089659918426, 70.38908280829822672 ) ) ;
#20281=DIRECTION ( 'NONE',  ( 1.000000000000000000, 3.387630566026860322E-15, -1.224646799147353207E-16 ) ) ;
#20341=VECTOR ( 'NONE', #18626, 1000.000000000000000 ) ;
#20358=DIRECTION ( 'NONE',  ( -1.000000000000000000, 0.000000000000000000, 0.000000000000000000 ) ) ;
#20368=EDGE_CURVE ( 'NONE', #8087, #9625, #2841, .T. ) ;
#20371=CARTESIAN_POINT ( 'NONE',  ( -9.178906393579158163, 42.46645089659918426, 67.75164986378473486 ) ) ;
#20494=LINE ( 'NONE', #3, #5165 ) ;
#20517=DIRECTION ( 'NONE',  ( -1.224646799147353207E-16, -0.000000000000000000, -1.000000000000000000 ) ) ;
#20527=DIRECTION ( 'NONE',  ( 1.224646799147353207E-16, 0.000000000000000000, 1.000000000000000000 ) ) ;
#20554=PLANE ( 'NONE',  #2045 ) ;
#20597=CONICAL_SURFACE ( 'NONE', #1271, 3077.683537175317724, 1.256637061435923464 ) ;
#20601=VERTEX_POINT ( 'NONE', #15883 ) ;
#20605=VECTOR ( 'NONE', #17796, 1000.000000000000000 ) ;
#20633=EDGE_LOOP ( 'NONE', ( #21415, #13727, #18494, #15244 ) ) ;
#20655=AXIS2_PLACEMENT_3D ( 'NONE', #6822, #12143, #15173 ) ;
#20664=ORIENTED_EDGE ( 'NONE', *, *, #19303, .F. ) ;
#20678=DIRECTION ( 'NONE',  ( -1.327594496921025717E-16, -1.000000000000000000, 1.625834351219974904E-32 ) ) ;
#20681=LINE ( 'NONE', #20788, #14645 ) ;
#20691=PLANE ( 'NONE',  #21280 ) ;
#20724=CIRCLE ( 'NONE', #19279, 0.9652499999999990532 ) ;
#20741=CARTESIAN_POINT ( 'NONE',  ( -6.728906393579160650, 43.00645089659919762, 70.88527860057354246 ) ) ;
#20745=CARTESIAN_POINT ( 'NONE',  ( -6.678906393579157275, 42.46645089659918426, 67.85468508031152624 ) ) ;
#20750=DIRECTION ( 'NONE',  ( -1.000000000000000000, 0.000000000000000000, 0.000000000000000000 ) ) ;
#20775=DIRECTION ( 'NONE',  ( -1.224646799147353207E-16, 0.000000000000000000, -1.000000000000000000 ) ) ;
#20776=DIRECTION ( 'NONE',  ( -1.000000000000000000, 0.000000000000000000, 0.000000000000000000 ) ) ;
#20788=CARTESIAN_POINT ( 'NONE',  ( -8.638906393579159015, 40.01645089659919563, 70.88527860057354246 ) ) ;
#20802=VECTOR ( 'NONE', #10545, 1000.000000000000000 ) ;
#20816=PLANE ( 'NONE',  #15770 ) ;
#20820=ORIENTED_EDGE ( 'NONE', *, *, #3325, .T. ) ;
#20915=DIRECTION ( 'NONE',  ( 0.4461977533474359436, 1.454668808886071847E-15, -0.8949343913984424415 ) ) ;
#20949=DIRECTION ( 'NONE',  ( -1.224646799147353207E-16, -0.000000000000000000, -1.000000000000000000 ) ) ;
#20955=VERTEX_POINT ( 'NONE', #1086 ) ;
#20958=( NAMED_UNIT ( * ) PLANE_ANGLE_UNIT ( ) SI_UNIT ( $, .RADIAN. ) );
#20996=FACE_OUTER_BOUND ( 'NONE', #10780, .T. ) ;
#21025=CARTESIAN_POINT ( 'NONE',  ( -8.134906293162361024, 41.92645089659918511, 68.06527860057354928 ) ) ;
#21060=ORIENTED_EDGE ( 'NONE', *, *, #4283, .F. ) ;
#21082=DIRECTION ( 'NONE',  ( -1.224646799147353207E-16, -1.000000000000000000, 1.499759782661857608E-32 ) ) ;
#21107=ORIENTED_EDGE ( 'NONE', *, *, #10827, .T. ) ;
#21132=SURFACE_STYLE_USAGE ( .BOTH. , #5579 ) ;
#21138=CARTESIAN_POINT ( 'NONE',  ( -9.178906393579158163, 42.46645089659918426, 70.88527860057354246 ) ) ;
#21186=VECTOR ( 'NONE', #11264, 1000.000000000000000 ) ;
#21190=PLANE ( 'NONE',  #16655 ) ;
#21233=ADVANCED_FACE ( 'NONE', ( #17084 ), #1759, .T. ) ;
#21235=VERTEX_POINT ( 'NONE', #17188 ) ;
#21264=ADVANCED_FACE ( 'NONE', ( #20996 ), #5890, .T. ) ;
#21272=DIRECTION ( 'NONE',  ( -1.000000000000000000, 0.000000000000000000, 0.000000000000000000 ) ) ;
#21280=AXIS2_PLACEMENT_3D ( 'NONE', #3677, #10496, #17303 ) ;
#21307=EDGE_CURVE ( 'NONE', #14817, #9924, #15003, .T. ) ;
#21323=ORIENTED_EDGE ( 'NONE', *, *, #14662, .T. ) ;
#21358=ORIENTED_EDGE ( 'NONE', *, *, #5313, .T. ) ;
#21382=CIRCLE ( 'NONE', #2797, 1.250000000000000222 ) ;
#21390=VERTEX_POINT ( 'NONE', #21447 ) ;
#21415=ORIENTED_EDGE ( 'NONE', *, *, #7717, .F. ) ;
#21447=CARTESIAN_POINT ( 'NONE',  ( -9.718906393579157310, 40.01645089659919563, 70.88527860057354246 ) ) ;
#21451=CARTESIAN_POINT ( 'NONE',  ( -10.22290649399594642, 41.92645089659918511, 68.06527860057354928 ) ) ;
#21467=CIRCLE ( 'NONE', #2143, 2.881677036926254765 ) ;
#21503=EDGE_CURVE ( 'NONE', #3965, #14817, #6334, .T. ) ;
#21543=DIRECTION ( 'NONE',  ( -1.224646799147353207E-16, -0.000000000000000000, -1.000000000000000000 ) ) ;
#21571=CARTESIAN_POINT ( 'NONE',  ( -4.603906393579157097, 42.46645089659918426, 74.06027860057353962 ) ) ;
#21594=ORIENTED_EDGE ( 'NONE', *, *, #21307, .T. ) ;
#21605=CARTESIAN_POINT ( 'NONE',  ( -10.22290649399594642, 41.92645089659918511, 68.06527860057354928 ) ) ;
#21606=FACE_OUTER_BOUND ( 'NONE', #1351, .T. ) ;
#21631=VERTEX_POINT ( 'NONE', #8231 ) ;
#21634=UNCERTAINTY_MEASURE_WITH_UNIT (LENGTH_MEASURE( 1.000000000000000082E-05 ), #17635, 'distance_accuracy_value', 'NONE');
#21639=AXIS2_PLACEMENT_3D ( 'NONE', #15310, #11827, #16760 ) ;
#21705=ORIENTED_EDGE ( 'NONE', *, *, #22130, .F. ) ;
#21731=CARTESIAN_POINT ( 'NONE',  ( -9.718906393579157310, 41.66638367286108746, 68.06527860057354928 ) ) ;
#21733=EDGE_CURVE ( 'NONE', #183, #16035, #4372, .T. ) ;
#21799=ORIENTED_EDGE ( 'NONE', *, *, #18101, .T. ) ;
#21842=AXIS2_PLACEMENT_3D ( 'NONE', #11244, #14821, #2639 ) ;
#21846=CARTESIAN_POINT ( 'NONE',  ( -9.178906393579158163, 42.46645089659918426, 68.06527860057354928 ) ) ;
#21892=EDGE_LOOP ( 'NONE', ( #6161, #1184, #20007, #15346 ) ) ;
#21904=ADVANCED_FACE ( 'NONE', ( #2534 ), #19879, .T. ) ;
#21929=ORIENTED_EDGE ( 'NONE', *, *, #8939, .F. ) ;
#21986=AXIS2_PLACEMENT_3D ( 'NONE', #2594, #12864, #19384 ) ;
#22027=CARTESIAN_POINT ( 'NONE',  ( -8.638906393579159015, 43.51045099701597252, 68.06527860057354928 ) ) ;
#22029=DIRECTION ( 'NONE',  ( 1.224646799147353207E-16, 0.000000000000000000, 1.000000000000000000 ) ) ;
#22035=TOROIDAL_SURFACE ( 'NONE', #12343, 3.750000000000000000, 1.250000000000000000 ) ;
#22055=DIRECTION ( 'NONE',  ( -3.491481338843133355E-15, 1.000000000000000000, 4.275831445896958607E-31 ) ) ;
#22112=VERTEX_POINT ( 'NONE', #7306 ) ;
#22124=FACE_OUTER_BOUND ( 'NONE', #9696, .T. ) ;
#22127=AXIS2_PLACEMENT_3D ( 'NONE', #18046, #19748, #5885 ) ;
#22130=EDGE_CURVE ( 'NONE', #20601, #13526, #16775, .T. ) ;
#22154=FACE_OUTER_BOUND ( 'NONE', #20633, .T. ) ;
ENDSEC;
END-ISO-10303-21;
